ISO-10303-21;
HEADER;
/* Generated by software containing ST-Developer
 * from STEP Tools, Inc. (www.steptools.com) 
 */

FILE_DESCRIPTION(
/* description */ ('Pipe clamp stand with threaded column'),
/* implementation_level */ '2;1');

FILE_NAME(
/* name */ 'M24 adjustment nut (1).step',
/* time_stamp */ '2026-10-27T10:55:48-07:00',
/* author */ (''),
/* organization */ (''),
/* preprocessor_version */ 'ST-DEVELOPER v20.2',
/* originating_system */ 'Autodesk Translation Framework v15.17.0.0',
/* authorisation */ '');

FILE_SCHEMA (('AUTOMOTIVE_DESIGN { 1 0 10303 214 3 1 1 }'));
ENDSEC;

DATA;
#10=MECHANICAL_DESIGN_GEOMETRIC_PRESENTATION_REPRESENTATION('',(#768),#34433);
#211=B_SPLINE_SURFACE_WITH_KNOTS('',3,3,((#30749,#30750,#30751,#30752,#30753,
#30754,#30755,#30756,#30757,#30758,#30759,#30760,#30761,#30762,#30763,#30764,
#30765,#30766,#30767,#30768,#30769,#30770,#30771,#30772,#30773,#30774,#30775,
#30776,#30777,#30778,#30779,#30780,#30781,#30782,#30783,#30784,#30785,#30786,
#30787,#30788,#30789,#30790,#30791,#30792,#30793,#30794,#30795,#30796,#30797,
#30798,#30799,#30800,#30801,#30802,#30803,#30804,#30805,#30806,#30807),
(#30808,#30809,#30810,#30811,#30812,#30813,#30814,#30815,#30816,#30817,
#30818,#30819,#30820,#30821,#30822,#30823,#30824,#30825,#30826,#30827,#30828,
#30829,#30830,#30831,#30832,#30833,#30834,#30835,#30836,#30837,#30838,#30839,
#30840,#30841,#30842,#30843,#30844,#30845,#30846,#30847,#30848,#30849,#30850,
#30851,#30852,#30853,#30854,#30855,#30856,#30857,#30858,#30859,#30860,#30861,
#30862,#30863,#30864,#30865,#30866),(#30867,#30868,#30869,#30870,#30871,
#30872,#30873,#30874,#30875,#30876,#30877,#30878,#30879,#30880,#30881,#30882,
#30883,#30884,#30885,#30886,#30887,#30888,#30889,#30890,#30891,#30892,#30893,
#30894,#30895,#30896,#30897,#30898,#30899,#30900,#30901,#30902,#30903,#30904,
#30905,#30906,#30907,#30908,#30909,#30910,#30911,#30912,#30913,#30914,#30915,
#30916,#30917,#30918,#30919,#30920,#30921,#30922,#30923,#30924,#30925),
(#30926,#30927,#30928,#30929,#30930,#30931,#30932,#30933,#30934,#30935,
#30936,#30937,#30938,#30939,#30940,#30941,#30942,#30943,#30944,#30945,#30946,
#30947,#30948,#30949,#30950,#30951,#30952,#30953,#30954,#30955,#30956,#30957,
#30958,#30959,#30960,#30961,#30962,#30963,#30964,#30965,#30966,#30967,#30968,
#30969,#30970,#30971,#30972,#30973,#30974,#30975,#30976,#30977,#30978,#30979,
#30980,#30981,#30982,#30983,#30984)),.UNSPECIFIED.,.F.,.F.,.F.,(4,4),(4,
1,1,1,1,1,1,1,1,1,1,1,1,1,1,1,1,1,1,1,1,1,1,1,1,1,1,1,1,1,1,1,1,1,1,1,1,
1,1,1,1,1,1,1,1,1,1,1,1,1,1,1,1,1,1,1,4),(0.,0.193239135097767),(11.852035964745,
12.3369705490203,12.8219051332956,13.3068397175709,13.7917743018461,14.2767088861214,
14.7616434703967,15.246578054672,15.7315126389472,16.2164472232225,16.7013818074978,
17.1863163917731,17.6712509760483,18.1561855603236,18.6411201445989,19.1260547288742,
19.6109893131495,20.0959238974247,20.5808584817,21.0657930659753,21.5507276502506,
22.0356622345258,22.5205968188011,23.0055314030764,23.4904659873517,23.9754005716269,
24.4603351559022,24.9452697401775,25.4302043244528,25.9151389087281,26.4000734930033,
26.8850080772786,27.3699426615539,27.8548772458292,28.3398118301044,28.8247464143797,
29.309680998655,29.7946155829303,30.2795501672055,30.7644847514808,31.2494193357561,
31.7343539200314,32.2192885043067,32.7042230885819,33.1891576728572,33.6740922571325,
34.1590268414078,34.643961425683,35.1288960099583,35.6138305942336,36.0987651785089,
36.5836997627841,37.0686343470594,37.5535689313347,38.03850351561,38.5234380998853,
39.0083726841605),.UNSPECIFIED.);
#212=B_SPLINE_SURFACE_WITH_KNOTS('',3,3,((#31183,#31184,#31185,#31186,#31187,
#31188,#31189,#31190,#31191,#31192,#31193,#31194,#31195,#31196,#31197,#31198,
#31199,#31200,#31201,#31202,#31203,#31204,#31205,#31206,#31207,#31208,#31209,
#31210,#31211,#31212,#31213,#31214,#31215,#31216,#31217,#31218,#31219,#31220,
#31221,#31222,#31223,#31224,#31225,#31226,#31227,#31228,#31229,#31230,#31231,
#31232,#31233,#31234,#31235,#31236,#31237,#31238,#31239,#31240,#31241),
(#31242,#31243,#31244,#31245,#31246,#31247,#31248,#31249,#31250,#31251,
#31252,#31253,#31254,#31255,#31256,#31257,#31258,#31259,#31260,#31261,#31262,
#31263,#31264,#31265,#31266,#31267,#31268,#31269,#31270,#31271,#31272,#31273,
#31274,#31275,#31276,#31277,#31278,#31279,#31280,#31281,#31282,#31283,#31284,
#31285,#31286,#31287,#31288,#31289,#31290,#31291,#31292,#31293,#31294,#31295,
#31296,#31297,#31298,#31299,#31300),(#31301,#31302,#31303,#31304,#31305,
#31306,#31307,#31308,#31309,#31310,#31311,#31312,#31313,#31314,#31315,#31316,
#31317,#31318,#31319,#31320,#31321,#31322,#31323,#31324,#31325,#31326,#31327,
#31328,#31329,#31330,#31331,#31332,#31333,#31334,#31335,#31336,#31337,#31338,
#31339,#31340,#31341,#31342,#31343,#31344,#31345,#31346,#31347,#31348,#31349,
#31350,#31351,#31352,#31353,#31354,#31355,#31356,#31357,#31358,#31359),
(#31360,#31361,#31362,#31363,#31364,#31365,#31366,#31367,#31368,#31369,
#31370,#31371,#31372,#31373,#31374,#31375,#31376,#31377,#31378,#31379,#31380,
#31381,#31382,#31383,#31384,#31385,#31386,#31387,#31388,#31389,#31390,#31391,
#31392,#31393,#31394,#31395,#31396,#31397,#31398,#31399,#31400,#31401,#31402,
#31403,#31404,#31405,#31406,#31407,#31408,#31409,#31410,#31411,#31412,#31413,
#31414,#31415,#31416,#31417,#31418)),.UNSPECIFIED.,.F.,.F.,.F.,(4,4),(4,
1,1,1,1,1,1,1,1,1,1,1,1,1,1,1,1,1,1,1,1,1,1,1,1,1,1,1,1,1,1,1,1,1,1,1,1,
1,1,1,1,1,1,1,1,1,1,1,1,1,1,1,1,1,1,1,4),(0.,0.193239135097767),(14.398702426866,
14.8836370111412,15.3685715954165,15.8535061796918,16.3384407639671,16.8233753482423,
17.3083099325176,17.7932445167929,18.2781791010682,18.7631136853434,19.2480482696187,
19.732982853894,20.2179174381693,20.7028520224446,21.1877866067198,21.6727211909951,
22.1576557752704,22.6425903595457,23.1275249438209,23.6124595280962,24.0973941123715,
24.5823286966468,25.0672632809221,25.5521978651973,26.0371324494726,26.5220670337479,
27.0070016180232,27.4919362022984,27.9768707865737,28.461805370849,28.9467399551243,
29.4316745393996,29.9166091236748,30.4015437079501,30.8864782922254,31.3714128765007,
31.8563474607759,32.3412820450512,32.8262166293265,33.3111512136018,33.796085797877,
34.2810203821523,34.7659549664276,35.2508895507029,35.7358241349782,36.2207587192534,
36.7056933035287,37.190627887804,37.6755624720793,38.1604970563545,38.6454316406298,
39.1303662249051,39.6153008091804,40.1002353934557,40.5851699777309,41.0701045620062,
41.5550391462815),.UNSPECIFIED.);
#625=B_SPLINE_CURVE_WITH_KNOTS('',3,(#30307,#30308,#30309,#30310,#30311,
#30312,#30313),.UNSPECIFIED.,.F.,.F.,(4,3,4),(26.4420020698014,26.6714021351403,
27.1563367194155),.UNSPECIFIED.);
#626=B_SPLINE_CURVE_WITH_KNOTS('',3,(#30316,#30317,#30318,#30319,#30320,
#30321,#30322,#30323,#30324,#30325,#30326,#30327,#30328,#30329,#30330,#30331,
#30332,#30333,#30334),.UNSPECIFIED.,.F.,.F.,(4,3,3,3,3,3,4),(-25.1327412287182,
-24.7316637980391,-24.2467292137639,-23.7617946294886,-23.2768600452133,
-22.791925460938,-22.7054832247427),.UNSPECIFIED.);
#627=B_SPLINE_CURVE_WITH_KNOTS('',3,(#30339,#30340,#30341,#30342,#30343,
#30344,#30345,#30346,#30347,#30348,#30349,#30350,#30351,#30352,#30353,#30354,
#30355,#30356,#30357,#30358,#30359,#30360,#30361,#30362,#30363,#30364,#30365,
#30366,#30367,#30368,#30369,#30370,#30371,#30372,#30373,#30374,#30375,#30376,
#30377,#30378,#30379,#30380,#30381),.UNSPECIFIED.,.F.,.F.,(4,3,3,3,3,3,
3,3,3,3,3,3,3,3,4),(20.1588167626218,20.3672525395616,20.8521871238369,
21.3371217081122,21.8220562923875,22.3069908766628,22.791925460938,23.2768600452133,
23.7617946294886,24.2467292137639,24.7316637980392,25.2165983823144,25.7015329665897,
26.186467550865,26.4420020698014),.UNSPECIFIED.);
#628=B_SPLINE_CURVE_WITH_KNOTS('',3,(#30382,#30383,#30384,#30385,#30386,
#30387,#30388,#30389,#30390,#30391,#30392,#30393,#30394,#30395,#30396,#30397,
#30398,#30399,#30400,#30401,#30402,#30403,#30404,#30405,#30406,#30407,#30408,
#30409,#30410,#30411,#30412,#30413,#30414,#30415,#30416,#30417,#30418,#30419,
#30420,#30421,#30422,#30423,#30424),.UNSPECIFIED.,.F.,.F.,(4,3,3,3,3,3,
3,3,3,3,3,3,3,3,4),(-22.7054832247427,-22.3069908766627,-21.8220562923875,
-21.3371217081122,-20.8521871238369,-20.3672525395616,-19.8823179552864,
-19.3973833710111,-18.9124487867358,-18.4275142024605,-17.9425796181852,
-17.45764503391,-16.9727104496347,-16.4877758653594,-16.4222979175631),
 .UNSPECIFIED.);
#629=B_SPLINE_CURVE_WITH_KNOTS('',3,(#30429,#30430,#30431,#30432,#30433,
#30434,#30435,#30436,#30437,#30438,#30439,#30440,#30441,#30442,#30443,#30444,
#30445,#30446,#30447,#30448,#30449,#30450,#30451,#30452,#30453,#30454,#30455,
#30456,#30457,#30458,#30459,#30460,#30461,#30462,#30463,#30464,#30465,#30466,
#30467,#30468,#30469,#30470,#30471),.UNSPECIFIED.,.F.,.F.,(4,3,3,3,3,3,
3,3,3,3,3,3,3,3,4),(13.8756314554422,14.063102943983,14.5480375282583,15.0329721125336,
15.5179066968089,16.0028412810842,16.4877758653594,16.9727104496347,17.45764503391,
17.9425796181853,18.4275142024605,18.9124487867358,19.3973833710111,19.8823179552864,
20.1588167626218),.UNSPECIFIED.);
#630=B_SPLINE_CURVE_WITH_KNOTS('',3,(#30472,#30473,#30474,#30475,#30476,
#30477,#30478,#30479,#30480,#30481,#30482,#30483,#30484,#30485,#30486,#30487,
#30488,#30489,#30490,#30491,#30492,#30493,#30494,#30495,#30496,#30497,#30498,
#30499,#30500,#30501,#30502,#30503,#30504,#30505,#30506,#30507,#30508,#30509,
#30510,#30511,#30512,#30513,#30514),.UNSPECIFIED.,.F.,.F.,(4,3,3,3,3,3,
3,3,3,3,3,3,3,3,4),(-16.4222979175631,-16.0028412810841,-15.5179066968089,
-15.0329721125336,-14.5480375282583,-14.063102943983,-13.5781683597078,
-13.0932337754325,-12.6082991911572,-12.1233646068819,-11.6384300226066,
-11.1534954383314,-10.6685608540561,-10.1836262697808,-10.1391126103836),
 .UNSPECIFIED.);
#631=B_SPLINE_CURVE_WITH_KNOTS('',3,(#30520,#30521,#30522,#30523,#30524,
#30525,#30526,#30527,#30528,#30529,#30530,#30531,#30532,#30533,#30534,#30535,
#30536,#30537,#30538,#30539,#30540,#30541,#30542,#30543,#30544),
 .UNSPECIFIED.,.F.,.F.,(4,3,3,3,3,3,3,3,4),(-3.85592730320397,-3.39454208992694,
-2.90960750565166,-2.42467292137638,-1.93973833710111,-1.45480375282583,
-0.969869168550556,-0.484934584275276,0.),.UNSPECIFIED.);
#632=B_SPLINE_CURVE_WITH_KNOTS('',3,(#30547,#30548,#30549,#30550,#30551,
#30552,#30553,#30554,#30555,#30556,#30557,#30558,#30559,#30560,#30561,#30562,
#30563,#30564,#30565,#30566,#30567,#30568,#30569,#30570,#30571,#30572,#30573,
#30574,#30575,#30576,#30577,#30578,#30579,#30580,#30581,#30582,#30583),
 .UNSPECIFIED.,.F.,.F.,(4,3,3,3,3,3,3,3,3,3,3,3,4),(2.02359549069725,2.42467292137638,
2.90960750565166,3.39454208992694,3.87947667420222,4.36441125847749,4.84934584275277,
5.33428042702805,5.81921501130332,6.3041495955786,6.78908417985388,7.27401876412916,
7.59244614826257),.UNSPECIFIED.);
#633=B_SPLINE_CURVE_WITH_KNOTS('',3,(#30589,#30590,#30591,#30592,#30593,
#30594,#30595,#30596,#30597,#30598,#30599,#30600,#30601),.UNSPECIFIED.,
 .F.,.F.,(4,1,1,1,1,1,1,1,1,1,4),(34.5575191894877,34.643961425683,35.1288960099583,
35.6138305942336,36.0987651785089,36.5836997627841,37.0686343470594,37.5535689313347,
38.03850351561,38.5234380998853,39.0083726841605),.UNSPECIFIED.);
#634=B_SPLINE_CURVE_WITH_KNOTS('',3,(#30604,#30605,#30606,#30607,#30608,
#30609,#30610,#30611,#30612,#30613,#30614,#30615,#30616,#30617),
 .UNSPECIFIED.,.F.,.F.,(4,1,1,1,1,1,1,1,1,1,1,4),(34.5575191894877,34.7659549664276,
35.2508895507029,35.7358241349782,36.2207587192534,36.7056933035287,37.190627887804,
37.6755624720793,38.1604970563545,38.6454316406298,39.1303662249051,39.5314436555842),
 .UNSPECIFIED.);
#635=B_SPLINE_CURVE_WITH_KNOTS('',3,(#30622,#30623,#30624,#30625,#30626,
#30627,#30628,#30629,#30630,#30631,#30632,#30633,#30634,#30635,#30636,#30637,
#30638),.UNSPECIFIED.,.F.,.F.,(4,1,1,1,1,1,1,1,1,1,1,1,1,1,4),(28.2743338823081,
28.3398118301044,28.8247464143797,29.309680998655,29.7946155829303,30.2795501672055,
30.7644847514808,31.2494193357561,31.7343539200314,32.2192885043067,32.7042230885819,
33.1891576728572,33.6740922571325,34.1590268414078,34.5575191894877),
 .UNSPECIFIED.);
#636=B_SPLINE_CURVE_WITH_KNOTS('',3,(#30639,#30640,#30641,#30642,#30643,
#30644,#30645,#30646,#30647,#30648,#30649,#30650,#30651,#30652,#30653,#30654,
#30655),.UNSPECIFIED.,.F.,.F.,(4,1,1,1,1,1,1,1,1,1,1,1,1,1,4),(28.2743338823081,
28.461805370849,28.9467399551243,29.4316745393996,29.9166091236748,30.4015437079501,
30.8864782922254,31.3714128765007,31.8563474607759,32.3412820450512,32.8262166293265,
33.3111512136018,33.796085797877,34.2810203821523,34.5575191894877),
 .UNSPECIFIED.);
#637=B_SPLINE_CURVE_WITH_KNOTS('',3,(#30660,#30661,#30662,#30663,#30664,
#30665,#30666,#30667,#30668,#30669,#30670,#30671,#30672,#30673,#30674,#30675,
#30676),.UNSPECIFIED.,.F.,.F.,(4,1,1,1,1,1,1,1,1,1,1,1,1,1,4),(21.9911485751285,
22.0356622345258,22.5205968188011,23.0055314030764,23.4904659873517,23.9754005716269,
24.4603351559022,24.9452697401775,25.4302043244528,25.9151389087281,26.4000734930033,
26.8850080772786,27.3699426615539,27.8548772458292,28.2743338823081),
 .UNSPECIFIED.);
#638=B_SPLINE_CURVE_WITH_KNOTS('',3,(#30677,#30678,#30679,#30680,#30681,
#30682,#30683,#30684,#30685,#30686,#30687,#30688,#30689,#30690,#30691,#30692,
#30693),.UNSPECIFIED.,.F.,.F.,(4,1,1,1,1,1,1,1,1,1,1,1,1,1,4),(21.9911485751285,
22.1576557752704,22.6425903595457,23.1275249438209,23.6124595280962,24.0973941123715,
24.5823286966468,25.0672632809221,25.5521978651973,26.0371324494726,26.5220670337479,
27.0070016180232,27.4919362022984,27.9768707865737,28.2743338823081),
 .UNSPECIFIED.);
#639=B_SPLINE_CURVE_WITH_KNOTS('',3,(#30699,#30700,#30701,#30702,#30703,
#30704),.UNSPECIFIED.,.F.,.F.,(4,1,1,4),(14.398702426866,14.8836370111412,
15.3685715954165,15.707963267949),.UNSPECIFIED.);
#640=B_SPLINE_CURVE_WITH_KNOTS('',3,(#30707,#30708,#30709,#30710,#30711,
#30712,#30713),.UNSPECIFIED.,.F.,.F.,(4,1,1,1,4),(13.8756314554423,14.2767088861214,
14.7616434703967,15.246578054672,15.707963267949),.UNSPECIFIED.);
#641=B_SPLINE_CURVE_WITH_KNOTS('',3,(#30715,#30716,#30717,#30718,#30719,
#30720,#30721,#30722,#30723,#30724,#30725,#30726,#30727,#30728,#30729,#30730,
#30731),.UNSPECIFIED.,.F.,.F.,(4,1,1,1,1,1,1,1,1,1,1,1,1,1,4),(15.707963267949,
15.7315126389472,16.2164472232225,16.7013818074978,17.1863163917731,17.6712509760483,
18.1561855603236,18.6411201445989,19.1260547288742,19.6109893131495,20.0959238974247,
20.5808584817,21.0657930659753,21.5507276502506,21.9911485751285),
 .UNSPECIFIED.);
#642=B_SPLINE_CURVE_WITH_KNOTS('',3,(#30732,#30733,#30734,#30735,#30736,
#30737,#30738,#30739,#30740,#30741,#30742,#30743,#30744,#30745,#30746,#30747,
#30748),.UNSPECIFIED.,.F.,.F.,(4,1,1,1,1,1,1,1,1,1,1,1,1,1,4),(15.707963267949,
15.8535061796918,16.3384407639671,16.8233753482423,17.3083099325176,17.7932445167929,
18.2781791010682,18.7631136853434,19.2480482696187,19.732982853894,20.2179174381693,
20.7028520224446,21.1877866067198,21.6727211909951,21.9911485751285),
 .UNSPECIFIED.);
#643=B_SPLINE_CURVE_WITH_KNOTS('',3,(#30985,#30986,#30987,#30988,#30989,
#30990,#30991,#30992,#30993,#30994,#30995,#30996,#30997,#30998,#30999,#31000,
#31001,#31002,#31003,#31004,#31005,#31006,#31007,#31008,#31009,#31010,#31011,
#31012,#31013,#31014,#31015,#31016,#31017,#31018,#31019,#31020,#31021,#31022,
#31023,#31024,#31025,#31026,#31027,#31028,#31029,#31030,#31031,#31032,#31033,
#31034,#31035,#31036,#31037,#31038,#31039,#31040,#31041,#31042,#31043,#31044,
#31045,#31046,#31047,#31048,#31049,#31050,#31051,#31052,#31053,#31054,#31055,
#31056,#31057,#31058,#31059,#31060,#31061,#31062,#31063),.UNSPECIFIED.,
 .F.,.F.,(4,3,3,3,3,3,3,3,3,3,3,3,3,3,3,3,3,3,3,3,3,3,3,3,3,3,4),(0.,0.152217036456305,
0.304359559108715,0.444170424706737,0.471986618924989,0.583981290304758,
0.733405166385902,0.837349491605518,0.892796377491797,0.921013022333204,
0.951233782076786,1.09712080302743,1.14918246726436,1.28571136325167,1.34308236504369,
1.37129895791557,1.51452713235171,1.65613248204747,1.6952980512136,1.76334985118988,
1.79789349372615,1.82919285548252,1.96987771326252,2.04822493259179,2.08147550163167,
2.22116640322437,2.31010750305869),.UNSPECIFIED.);
#644=B_SPLINE_CURVE_WITH_KNOTS('',3,(#31064,#31065,#31066,#31067,#31068,
#31069,#31070,#31071,#31072,#31073,#31074,#31075,#31076,#31077,#31078,#31079,
#31080,#31081,#31082,#31083,#31084,#31085,#31086,#31087,#31088,#31089,#31090,
#31091,#31092,#31093,#31094,#31095,#31096,#31097,#31098,#31099,#31100,#31101,
#31102,#31103,#31104,#31105,#31106,#31107,#31108,#31109,#31110,#31111,#31112,
#31113,#31114,#31115,#31116,#31117,#31118,#31119,#31120,#31121,#31122,#31123,
#31124,#31125,#31126,#31127,#31128,#31129,#31130,#31131,#31132,#31133,#31134,
#31135,#31136,#31137,#31138,#31139),.UNSPECIFIED.,.F.,.F.,(4,3,3,3,3,3,
3,3,3,3,3,3,3,3,3,3,3,3,3,3,3,3,3,3,3,4),(0.,0.136945726883441,0.275843669299818,
0.398833938019505,0.433644951757236,0.521824206739191,0.663225099265181,
0.763150397883695,0.825065214142751,0.86108829768601,1.00600626575755,1.06292629373924,
1.2029565761277,1.26303420019935,1.30095883535296,1.44786419265016,1.59611026313033,
1.6230474232931,1.69648824397694,1.73120198878345,1.76336660816569,1.9136029124139,
1.9976034301376,2.04132623841743,2.20106314648746,2.30292298333827),
 .UNSPECIFIED.);
#645=B_SPLINE_CURVE_WITH_KNOTS('',3,(#31140,#31141,#31142,#31143,#31144,
#31145,#31146,#31147,#31148,#31149,#31150,#31151,#31152,#31153,#31154,#31155,
#31156,#31157,#31158,#31159,#31160,#31161,#31162,#31163,#31164,#31165,#31166,
#31167,#31168,#31169,#31170,#31171,#31172,#31173,#31174,#31175,#31176,#31177,
#31178,#31179,#31180,#31181,#31182),.UNSPECIFIED.,.F.,.F.,(4,3,3,3,3,3,
3,3,3,3,3,3,3,3,4),(-10.1391126103836,-9.69869168550554,-9.21375710123026,
-8.72882251695498,-8.24388793267971,-7.75895334840443,-7.27401876412915,
-6.78908417985388,-6.3041495955786,-5.81921501130332,-5.33428042702805,
-4.84934584275277,-4.36441125847749,-3.87947667420222,-3.85592730320397),
 .UNSPECIFIED.);
#646=B_SPLINE_CURVE_WITH_KNOTS('',3,(#31419,#31420,#31421,#31422,#31423,
#31424,#31425,#31426,#31427,#31428,#31429,#31430,#31431,#31432,#31433,#31434,
#31435,#31436,#31437,#31438,#31439,#31440,#31441,#31442,#31443,#31444,#31445,
#31446,#31447,#31448,#31449,#31450,#31451,#31452,#31453,#31454,#31455,#31456,
#31457,#31458,#31459,#31460,#31461,#31462,#31463,#31464,#31465,#31466,#31467,
#31468,#31469,#31470,#31471,#31472,#31473,#31474,#31475,#31476,#31477,#31478,
#31479,#31480,#31481,#31482,#31483,#31484,#31485,#31486,#31487,#31488,#31489,
#31490,#31491,#31492,#31493,#31494),.UNSPECIFIED.,.F.,.F.,(4,3,3,3,3,3,
3,3,3,3,3,3,3,3,3,3,3,3,3,3,3,3,3,3,3,4),(0.,0.13694559794668,0.275843482121711,
0.398833844430455,0.433644934608767,0.521824206739199,0.663225163953675,
0.763150446400059,0.825065359497682,0.861088305549411,1.00600631943109,
1.06292629373921,1.20295657612767,1.26303420036263,1.30095883585408,1.44786417212767,
1.59611023917669,1.62304742329305,1.69648824478928,1.73120199734959,1.76336661014496,
1.91360291342174,1.99760343201209,2.04132623949843,2.20106314648734,2.30292298333806),
 .UNSPECIFIED.);
#647=B_SPLINE_CURVE_WITH_KNOTS('',3,(#31495,#31496,#31497,#31498,#31499,
#31500,#31501,#31502,#31503,#31504,#31505,#31506,#31507,#31508,#31509,#31510,
#31511,#31512,#31513,#31514,#31515,#31516,#31517,#31518,#31519,#31520,#31521,
#31522,#31523,#31524,#31525,#31526,#31527,#31528,#31529,#31530,#31531,#31532,
#31533,#31534,#31535,#31536,#31537),.UNSPECIFIED.,.F.,.F.,(4,3,3,3,3,3,
3,3,3,3,3,3,3,3,4),(7.59244614826257,7.75895334840444,8.24388793267971,
8.72882251695499,9.21375710123027,9.69869168550555,10.1836262697808,10.6685608540561,
11.1534954383314,11.6384300226067,12.1233646068819,12.6082991911572,13.0932337754325,
13.5781683597078,13.8756314554422),.UNSPECIFIED.);
#648=B_SPLINE_CURVE_WITH_KNOTS('',3,(#31538,#31539,#31540,#31541,#31542,
#31543,#31544,#31545,#31546,#31547,#31548,#31549,#31550,#31551,#31552,#31553,
#31554,#31555,#31556,#31557,#31558,#31559,#31560,#31561,#31562,#31563,#31564,
#31565,#31566,#31567,#31568,#31569,#31570,#31571,#31572,#31573,#31574,#31575,
#31576,#31577,#31578,#31579,#31580,#31581,#31582,#31583,#31584,#31585,#31586,
#31587,#31588,#31589,#31590,#31591,#31592,#31593,#31594,#31595,#31596,#31597,
#31598,#31599,#31600,#31601,#31602,#31603,#31604,#31605,#31606,#31607,#31608,
#31609,#31610,#31611,#31612,#31613,#31614,#31615,#31616),.UNSPECIFIED.,
 .F.,.F.,(4,3,3,3,3,3,3,3,3,3,3,3,3,3,3,3,3,3,3,3,3,3,3,3,3,3,4),(0.,0.152216987149307,
0.304359545775131,0.444170418039944,0.471986614921483,0.583981290304757,
0.733405173606566,0.837349497021023,0.892796401978486,0.921012950047068,
0.951233774221015,1.09712078868938,1.14918246726439,1.2857113632517,1.34308236856545,
1.37129896045007,1.51452713148655,1.65613247659821,1.69529805121362,1.76334985216405,
1.79789350346528,1.82919285775424,1.96987771686527,2.04822493836997,2.08147550729113,
2.22116640322435,2.31010750305867),.UNSPECIFIED.);
#716=SHAPE_REPRESENTATION_RELATIONSHIP('SRR','None',#34560,#738);
#738=ADVANCED_BREP_SHAPE_REPRESENTATION('',(#796),#34428);
#768=STYLED_ITEM('',(#34750),#796);
#796=MANIFOLD_SOLID_BREP('Body1',#8797);
#851=FACE_BOUND('',#2022,.T.);
#852=FACE_BOUND('',#2031,.T.);
#1020=PLANE('',#9660);
#1021=PLANE('',#9662);
#1022=PLANE('',#9663);
#1023=PLANE('',#9664);
#1024=PLANE('',#9665);
#1025=PLANE('',#9666);
#1026=PLANE('',#9667);
#1027=PLANE('',#9668);
#1471=FACE_OUTER_BOUND('',#2010,.T.);
#1472=FACE_OUTER_BOUND('',#2011,.T.);
#1473=FACE_OUTER_BOUND('',#2012,.T.);
#1474=FACE_OUTER_BOUND('',#2013,.T.);
#1475=FACE_OUTER_BOUND('',#2014,.T.);
#1476=FACE_OUTER_BOUND('',#2015,.T.);
#1477=FACE_OUTER_BOUND('',#2016,.T.);
#1478=FACE_OUTER_BOUND('',#2017,.T.);
#1479=FACE_OUTER_BOUND('',#2018,.T.);
#1480=FACE_OUTER_BOUND('',#2019,.T.);
#1481=FACE_OUTER_BOUND('',#2020,.T.);
#1482=FACE_OUTER_BOUND('',#2021,.T.);
#1483=FACE_OUTER_BOUND('',#2023,.T.);
#1484=FACE_OUTER_BOUND('',#2024,.T.);
#1485=FACE_OUTER_BOUND('',#2025,.T.);
#1486=FACE_OUTER_BOUND('',#2026,.T.);
#1487=FACE_OUTER_BOUND('',#2027,.T.);
#1488=FACE_OUTER_BOUND('',#2028,.T.);
#1489=FACE_OUTER_BOUND('',#2029,.T.);
#1490=FACE_OUTER_BOUND('',#2030,.T.);
#2010=EDGE_LOOP('',(#7675,#7676,#7677,#7678));
#2011=EDGE_LOOP('',(#7679,#7680,#7681,#7682));
#2012=EDGE_LOOP('',(#7683,#7684,#7685,#7686));
#2013=EDGE_LOOP('',(#7687,#7688,#7689,#7690));
#2014=EDGE_LOOP('',(#7691,#7692,#7693,#7694));
#2015=EDGE_LOOP('',(#7695,#7696,#7697,#7698));
#2016=EDGE_LOOP('',(#7699,#7700,#7701,#7702));
#2017=EDGE_LOOP('',(#7703,#7704,#7705,#7706));
#2018=EDGE_LOOP('',(#7707,#7708,#7709,#7710));
#2019=EDGE_LOOP('',(#7711,#7712,#7713,#7714,#7715,#7716,#7717,#7718,#7719,
#7720,#7721,#7722));
#2020=EDGE_LOOP('',(#7723,#7724,#7725,#7726,#7727,#7728,#7729,#7730,#7731,
#7732,#7733,#7734));
#2021=EDGE_LOOP('',(#7735,#7736,#7737,#7738,#7739,#7740));
#2022=EDGE_LOOP('',(#7741,#7742,#7743,#7744));
#2023=EDGE_LOOP('',(#7745,#7746,#7747,#7748));
#2024=EDGE_LOOP('',(#7749,#7750,#7751,#7752));
#2025=EDGE_LOOP('',(#7753,#7754,#7755,#7756));
#2026=EDGE_LOOP('',(#7757,#7758,#7759,#7760));
#2027=EDGE_LOOP('',(#7761,#7762,#7763,#7764));
#2028=EDGE_LOOP('',(#7765,#7766,#7767,#7768));
#2029=EDGE_LOOP('',(#7769,#7770,#7771,#7772));
#2030=EDGE_LOOP('',(#7773,#7774,#7775,#7776,#7777,#7778));
#2031=EDGE_LOOP('',(#7779,#7780,#7781,#7782));
#2615=LINE('',#30305,#3232);
#2616=LINE('',#30338,#3233);
#2617=LINE('',#30428,#3234);
#2618=LINE('',#30518,#3235);
#2619=LINE('',#30587,#3236);
#2620=LINE('',#30621,#3237);
#2621=LINE('',#30659,#3238);
#2622=LINE('',#30697,#3239);
#2623=LINE('',#31620,#3240);
#2624=LINE('',#31622,#3241);
#2625=LINE('',#31624,#3242);
#2626=LINE('',#31626,#3243);
#2627=LINE('',#31628,#3244);
#2628=LINE('',#31629,#3245);
#2629=LINE('',#31634,#3246);
#2630=LINE('',#31635,#3247);
#2631=LINE('',#31636,#3248);
#2632=LINE('',#31639,#3249);
#2633=LINE('',#31640,#3250);
#2634=LINE('',#31643,#3251);
#2635=LINE('',#31644,#3252);
#2636=LINE('',#31647,#3253);
#2637=LINE('',#31648,#3254);
#2638=LINE('',#31651,#3255);
#2639=LINE('',#31652,#3256);
#2640=LINE('',#31654,#3257);
#3232=VECTOR('',#11474,1.05);
#3233=VECTOR('',#11479,1.05);
#3234=VECTOR('',#11482,1.05);
#3235=VECTOR('',#11485,1.05);
#3236=VECTOR('',#11490,1.21745);
#3237=VECTOR('',#11495,1.21745);
#3238=VECTOR('',#11498,1.21745);
#3239=VECTOR('',#11501,1.21745);
#3240=VECTOR('',#11508,1.);
#3241=VECTOR('',#11509,1.);
#3242=VECTOR('',#11510,1.);
#3243=VECTOR('',#11511,1.);
#3244=VECTOR('',#11512,1.);
#3245=VECTOR('',#11513,1.);
#3246=VECTOR('',#11518,1.);
#3247=VECTOR('',#11519,1.);
#3248=VECTOR('',#11520,1.);
#3249=VECTOR('',#11523,1.);
#3250=VECTOR('',#11524,1.);
#3251=VECTOR('',#11527,1.);
#3252=VECTOR('',#11528,1.);
#3253=VECTOR('',#11531,1.);
#3254=VECTOR('',#11532,1.);
#3255=VECTOR('',#11535,1.);
#3256=VECTOR('',#11536,1.);
#3257=VECTOR('',#11539,1.);
#3432=CIRCLE('',#9648,1.0501);
#3433=CIRCLE('',#9652,1.0501);
#3434=CIRCLE('',#9654,1.21745);
#3435=CIRCLE('',#9658,1.21745);
#4162=VERTEX_POINT('',#30303);
#4163=VERTEX_POINT('',#30304);
#4164=VERTEX_POINT('',#30306);
#4165=VERTEX_POINT('',#30314);
#4166=VERTEX_POINT('',#30336);
#4167=VERTEX_POINT('',#30337);
#4168=VERTEX_POINT('',#30426);
#4169=VERTEX_POINT('',#30427);
#4170=VERTEX_POINT('',#30516);
#4171=VERTEX_POINT('',#30517);
#4172=VERTEX_POINT('',#30519);
#4173=VERTEX_POINT('',#30545);
#4174=VERTEX_POINT('',#30585);
#4175=VERTEX_POINT('',#30586);
#4176=VERTEX_POINT('',#30588);
#4177=VERTEX_POINT('',#30602);
#4178=VERTEX_POINT('',#30619);
#4179=VERTEX_POINT('',#30620);
#4180=VERTEX_POINT('',#30657);
#4181=VERTEX_POINT('',#30658);
#4182=VERTEX_POINT('',#30695);
#4183=VERTEX_POINT('',#30696);
#4184=VERTEX_POINT('',#30698);
#4185=VERTEX_POINT('',#30705);
#4186=VERTEX_POINT('',#31618);
#4187=VERTEX_POINT('',#31619);
#4188=VERTEX_POINT('',#31621);
#4189=VERTEX_POINT('',#31623);
#4190=VERTEX_POINT('',#31625);
#4191=VERTEX_POINT('',#31627);
#4192=VERTEX_POINT('',#31632);
#4193=VERTEX_POINT('',#31633);
#4194=VERTEX_POINT('',#31638);
#4195=VERTEX_POINT('',#31642);
#4196=VERTEX_POINT('',#31646);
#4197=VERTEX_POINT('',#31650);
#5351=EDGE_CURVE('',#4162,#4163,#2615,.T.);
#5352=EDGE_CURVE('',#4163,#4164,#625,.T.);
#5353=EDGE_CURVE('',#4165,#4164,#3432,.T.);
#5354=EDGE_CURVE('',#4165,#4162,#626,.T.);
#5355=EDGE_CURVE('',#4166,#4167,#2616,.T.);
#5356=EDGE_CURVE('',#4167,#4163,#627,.T.);
#5357=EDGE_CURVE('',#4162,#4166,#628,.T.);
#5358=EDGE_CURVE('',#4168,#4169,#2617,.T.);
#5359=EDGE_CURVE('',#4169,#4167,#629,.T.);
#5360=EDGE_CURVE('',#4166,#4168,#630,.T.);
#5361=EDGE_CURVE('',#4170,#4171,#2618,.T.);
#5362=EDGE_CURVE('',#4170,#4172,#631,.T.);
#5363=EDGE_CURVE('',#4173,#4172,#3433,.F.);
#5364=EDGE_CURVE('',#4173,#4171,#632,.T.);
#5365=EDGE_CURVE('',#4174,#4175,#2619,.T.);
#5366=EDGE_CURVE('',#4175,#4176,#633,.T.);
#5367=EDGE_CURVE('',#4177,#4176,#3434,.T.);
#5368=EDGE_CURVE('',#4174,#4177,#634,.T.);
#5369=EDGE_CURVE('',#4178,#4179,#2620,.T.);
#5370=EDGE_CURVE('',#4179,#4175,#635,.T.);
#5371=EDGE_CURVE('',#4178,#4174,#636,.T.);
#5372=EDGE_CURVE('',#4180,#4181,#2621,.T.);
#5373=EDGE_CURVE('',#4181,#4179,#637,.T.);
#5374=EDGE_CURVE('',#4180,#4178,#638,.T.);
#5375=EDGE_CURVE('',#4182,#4183,#2622,.T.);
#5376=EDGE_CURVE('',#4184,#4182,#639,.T.);
#5377=EDGE_CURVE('',#4185,#4184,#3435,.T.);
#5378=EDGE_CURVE('',#4185,#4183,#640,.T.);
#5379=EDGE_CURVE('',#4183,#4181,#641,.T.);
#5380=EDGE_CURVE('',#4182,#4180,#642,.T.);
#5381=EDGE_CURVE('',#4176,#4165,#643,.T.);
#5382=EDGE_CURVE('',#4172,#4185,#644,.T.);
#5383=EDGE_CURVE('',#4168,#4170,#645,.T.);
#5384=EDGE_CURVE('',#4164,#4177,#646,.T.);
#5385=EDGE_CURVE('',#4171,#4169,#647,.T.);
#5386=EDGE_CURVE('',#4184,#4173,#648,.T.);
#5387=EDGE_CURVE('',#4186,#4187,#2623,.T.);
#5388=EDGE_CURVE('',#4187,#4188,#2624,.T.);
#5389=EDGE_CURVE('',#4188,#4189,#2625,.T.);
#5390=EDGE_CURVE('',#4189,#4190,#2626,.T.);
#5391=EDGE_CURVE('',#4190,#4191,#2627,.T.);
#5392=EDGE_CURVE('',#4191,#4186,#2628,.T.);
#5393=EDGE_CURVE('',#4192,#4193,#2629,.T.);
#5394=EDGE_CURVE('',#4193,#4186,#2630,.T.);
#5395=EDGE_CURVE('',#4192,#4191,#2631,.T.);
#5396=EDGE_CURVE('',#4194,#4192,#2632,.T.);
#5397=EDGE_CURVE('',#4194,#4190,#2633,.T.);
#5398=EDGE_CURVE('',#4195,#4194,#2634,.T.);
#5399=EDGE_CURVE('',#4195,#4189,#2635,.T.);
#5400=EDGE_CURVE('',#4196,#4195,#2636,.T.);
#5401=EDGE_CURVE('',#4196,#4188,#2637,.T.);
#5402=EDGE_CURVE('',#4197,#4196,#2638,.T.);
#5403=EDGE_CURVE('',#4197,#4187,#2639,.T.);
#5404=EDGE_CURVE('',#4193,#4197,#2640,.T.);
#7675=ORIENTED_EDGE('',*,*,#5351,.T.);
#7676=ORIENTED_EDGE('',*,*,#5352,.T.);
#7677=ORIENTED_EDGE('',*,*,#5353,.F.);
#7678=ORIENTED_EDGE('',*,*,#5354,.T.);
#7679=ORIENTED_EDGE('',*,*,#5355,.T.);
#7680=ORIENTED_EDGE('',*,*,#5356,.T.);
#7681=ORIENTED_EDGE('',*,*,#5351,.F.);
#7682=ORIENTED_EDGE('',*,*,#5357,.T.);
#7683=ORIENTED_EDGE('',*,*,#5358,.T.);
#7684=ORIENTED_EDGE('',*,*,#5359,.T.);
#7685=ORIENTED_EDGE('',*,*,#5355,.F.);
#7686=ORIENTED_EDGE('',*,*,#5360,.T.);
#7687=ORIENTED_EDGE('',*,*,#5361,.F.);
#7688=ORIENTED_EDGE('',*,*,#5362,.T.);
#7689=ORIENTED_EDGE('',*,*,#5363,.F.);
#7690=ORIENTED_EDGE('',*,*,#5364,.T.);
#7691=ORIENTED_EDGE('',*,*,#5365,.T.);
#7692=ORIENTED_EDGE('',*,*,#5366,.T.);
#7693=ORIENTED_EDGE('',*,*,#5367,.F.);
#7694=ORIENTED_EDGE('',*,*,#5368,.F.);
#7695=ORIENTED_EDGE('',*,*,#5369,.T.);
#7696=ORIENTED_EDGE('',*,*,#5370,.T.);
#7697=ORIENTED_EDGE('',*,*,#5365,.F.);
#7698=ORIENTED_EDGE('',*,*,#5371,.F.);
#7699=ORIENTED_EDGE('',*,*,#5372,.T.);
#7700=ORIENTED_EDGE('',*,*,#5373,.T.);
#7701=ORIENTED_EDGE('',*,*,#5369,.F.);
#7702=ORIENTED_EDGE('',*,*,#5374,.F.);
#7703=ORIENTED_EDGE('',*,*,#5375,.F.);
#7704=ORIENTED_EDGE('',*,*,#5376,.F.);
#7705=ORIENTED_EDGE('',*,*,#5377,.F.);
#7706=ORIENTED_EDGE('',*,*,#5378,.T.);
#7707=ORIENTED_EDGE('',*,*,#5375,.T.);
#7708=ORIENTED_EDGE('',*,*,#5379,.T.);
#7709=ORIENTED_EDGE('',*,*,#5372,.F.);
#7710=ORIENTED_EDGE('',*,*,#5380,.F.);
#7711=ORIENTED_EDGE('',*,*,#5381,.F.);
#7712=ORIENTED_EDGE('',*,*,#5366,.F.);
#7713=ORIENTED_EDGE('',*,*,#5370,.F.);
#7714=ORIENTED_EDGE('',*,*,#5373,.F.);
#7715=ORIENTED_EDGE('',*,*,#5379,.F.);
#7716=ORIENTED_EDGE('',*,*,#5378,.F.);
#7717=ORIENTED_EDGE('',*,*,#5382,.F.);
#7718=ORIENTED_EDGE('',*,*,#5362,.F.);
#7719=ORIENTED_EDGE('',*,*,#5383,.F.);
#7720=ORIENTED_EDGE('',*,*,#5360,.F.);
#7721=ORIENTED_EDGE('',*,*,#5357,.F.);
#7722=ORIENTED_EDGE('',*,*,#5354,.F.);
#7723=ORIENTED_EDGE('',*,*,#5384,.F.);
#7724=ORIENTED_EDGE('',*,*,#5352,.F.);
#7725=ORIENTED_EDGE('',*,*,#5356,.F.);
#7726=ORIENTED_EDGE('',*,*,#5359,.F.);
#7727=ORIENTED_EDGE('',*,*,#5385,.F.);
#7728=ORIENTED_EDGE('',*,*,#5364,.F.);
#7729=ORIENTED_EDGE('',*,*,#5386,.F.);
#7730=ORIENTED_EDGE('',*,*,#5376,.T.);
#7731=ORIENTED_EDGE('',*,*,#5380,.T.);
#7732=ORIENTED_EDGE('',*,*,#5374,.T.);
#7733=ORIENTED_EDGE('',*,*,#5371,.T.);
#7734=ORIENTED_EDGE('',*,*,#5368,.T.);
#7735=ORIENTED_EDGE('',*,*,#5387,.T.);
#7736=ORIENTED_EDGE('',*,*,#5388,.T.);
#7737=ORIENTED_EDGE('',*,*,#5389,.T.);
#7738=ORIENTED_EDGE('',*,*,#5390,.T.);
#7739=ORIENTED_EDGE('',*,*,#5391,.T.);
#7740=ORIENTED_EDGE('',*,*,#5392,.T.);
#7741=ORIENTED_EDGE('',*,*,#5384,.T.);
#7742=ORIENTED_EDGE('',*,*,#5367,.T.);
#7743=ORIENTED_EDGE('',*,*,#5381,.T.);
#7744=ORIENTED_EDGE('',*,*,#5353,.T.);
#7745=ORIENTED_EDGE('',*,*,#5361,.T.);
#7746=ORIENTED_EDGE('',*,*,#5385,.T.);
#7747=ORIENTED_EDGE('',*,*,#5358,.F.);
#7748=ORIENTED_EDGE('',*,*,#5383,.T.);
#7749=ORIENTED_EDGE('',*,*,#5393,.T.);
#7750=ORIENTED_EDGE('',*,*,#5394,.T.);
#7751=ORIENTED_EDGE('',*,*,#5392,.F.);
#7752=ORIENTED_EDGE('',*,*,#5395,.F.);
#7753=ORIENTED_EDGE('',*,*,#5396,.T.);
#7754=ORIENTED_EDGE('',*,*,#5395,.T.);
#7755=ORIENTED_EDGE('',*,*,#5391,.F.);
#7756=ORIENTED_EDGE('',*,*,#5397,.F.);
#7757=ORIENTED_EDGE('',*,*,#5398,.T.);
#7758=ORIENTED_EDGE('',*,*,#5397,.T.);
#7759=ORIENTED_EDGE('',*,*,#5390,.F.);
#7760=ORIENTED_EDGE('',*,*,#5399,.F.);
#7761=ORIENTED_EDGE('',*,*,#5400,.T.);
#7762=ORIENTED_EDGE('',*,*,#5399,.T.);
#7763=ORIENTED_EDGE('',*,*,#5389,.F.);
#7764=ORIENTED_EDGE('',*,*,#5401,.F.);
#7765=ORIENTED_EDGE('',*,*,#5402,.T.);
#7766=ORIENTED_EDGE('',*,*,#5401,.T.);
#7767=ORIENTED_EDGE('',*,*,#5388,.F.);
#7768=ORIENTED_EDGE('',*,*,#5403,.F.);
#7769=ORIENTED_EDGE('',*,*,#5404,.T.);
#7770=ORIENTED_EDGE('',*,*,#5403,.T.);
#7771=ORIENTED_EDGE('',*,*,#5387,.F.);
#7772=ORIENTED_EDGE('',*,*,#5394,.F.);
#7773=ORIENTED_EDGE('',*,*,#5404,.F.);
#7774=ORIENTED_EDGE('',*,*,#5393,.F.);
#7775=ORIENTED_EDGE('',*,*,#5396,.F.);
#7776=ORIENTED_EDGE('',*,*,#5398,.F.);
#7777=ORIENTED_EDGE('',*,*,#5400,.F.);
#7778=ORIENTED_EDGE('',*,*,#5402,.F.);
#7779=ORIENTED_EDGE('',*,*,#5386,.T.);
#7780=ORIENTED_EDGE('',*,*,#5363,.T.);
#7781=ORIENTED_EDGE('',*,*,#5382,.T.);
#7782=ORIENTED_EDGE('',*,*,#5377,.T.);
#8251=CYLINDRICAL_SURFACE('',#9647,1.0501);
#8252=CYLINDRICAL_SURFACE('',#9649,1.0501);
#8253=CYLINDRICAL_SURFACE('',#9650,1.0501);
#8254=CYLINDRICAL_SURFACE('',#9651,1.0501);
#8255=CYLINDRICAL_SURFACE('',#9653,1.21745);
#8256=CYLINDRICAL_SURFACE('',#9655,1.21745);
#8257=CYLINDRICAL_SURFACE('',#9656,1.21745);
#8258=CYLINDRICAL_SURFACE('',#9657,1.21745);
#8259=CYLINDRICAL_SURFACE('',#9659,1.21745);
#8260=CYLINDRICAL_SURFACE('',#9661,1.0501);
#8708=ADVANCED_FACE('',(#1471),#8251,.F.);
#8709=ADVANCED_FACE('',(#1472),#8252,.F.);
#8710=ADVANCED_FACE('',(#1473),#8253,.F.);
#8711=ADVANCED_FACE('',(#1474),#8254,.F.);
#8712=ADVANCED_FACE('',(#1475),#8255,.F.);
#8713=ADVANCED_FACE('',(#1476),#8256,.F.);
#8714=ADVANCED_FACE('',(#1477),#8257,.F.);
#8715=ADVANCED_FACE('',(#1478),#8258,.F.);
#8716=ADVANCED_FACE('',(#1479),#8259,.F.);
#8717=ADVANCED_FACE('',(#1480),#211,.F.);
#8718=ADVANCED_FACE('',(#1481),#212,.F.);
#8719=ADVANCED_FACE('',(#1482,#851),#1020,.T.);
#8720=ADVANCED_FACE('',(#1483),#8260,.F.);
#8721=ADVANCED_FACE('',(#1484),#1021,.T.);
#8722=ADVANCED_FACE('',(#1485),#1022,.T.);
#8723=ADVANCED_FACE('',(#1486),#1023,.T.);
#8724=ADVANCED_FACE('',(#1487),#1024,.T.);
#8725=ADVANCED_FACE('',(#1488),#1025,.T.);
#8726=ADVANCED_FACE('',(#1489),#1026,.T.);
#8727=ADVANCED_FACE('',(#1490,#852),#1027,.F.);
#8797=CLOSED_SHELL('',(#8708,#8709,#8710,#8711,#8712,#8713,#8714,#8715,
#8716,#8717,#8718,#8719,#8720,#8721,#8722,#8723,#8724,#8725,#8726,#8727));
#9646=AXIS2_PLACEMENT_3D('',#30301,#11470,#11471);
#9647=AXIS2_PLACEMENT_3D('',#30302,#11472,#11473);
#9648=AXIS2_PLACEMENT_3D('',#30315,#11475,#11476);
#9649=AXIS2_PLACEMENT_3D('',#30335,#11477,#11478);
#9650=AXIS2_PLACEMENT_3D('',#30425,#11480,#11481);
#9651=AXIS2_PLACEMENT_3D('',#30515,#11483,#11484);
#9652=AXIS2_PLACEMENT_3D('',#30546,#11486,#11487);
#9653=AXIS2_PLACEMENT_3D('',#30584,#11488,#11489);
#9654=AXIS2_PLACEMENT_3D('',#30603,#11491,#11492);
#9655=AXIS2_PLACEMENT_3D('',#30618,#11493,#11494);
#9656=AXIS2_PLACEMENT_3D('',#30656,#11496,#11497);
#9657=AXIS2_PLACEMENT_3D('',#30694,#11499,#11500);
#9658=AXIS2_PLACEMENT_3D('',#30706,#11502,#11503);
#9659=AXIS2_PLACEMENT_3D('',#30714,#11504,#11505);
#9660=AXIS2_PLACEMENT_3D('',#31617,#11506,#11507);
#9661=AXIS2_PLACEMENT_3D('',#31630,#11514,#11515);
#9662=AXIS2_PLACEMENT_3D('',#31631,#11516,#11517);
#9663=AXIS2_PLACEMENT_3D('',#31637,#11521,#11522);
#9664=AXIS2_PLACEMENT_3D('',#31641,#11525,#11526);
#9665=AXIS2_PLACEMENT_3D('',#31645,#11529,#11530);
#9666=AXIS2_PLACEMENT_3D('',#31649,#11533,#11534);
#9667=AXIS2_PLACEMENT_3D('',#31653,#11537,#11538);
#9668=AXIS2_PLACEMENT_3D('',#31655,#11540,#11541);
#11470=DIRECTION('axis',(0.,0.,1.));
#11471=DIRECTION('refdir',(1.,0.,0.));
#11472=DIRECTION('center_axis',(0.,0.,1.));
#11473=DIRECTION('ref_axis',(1.,0.,0.));
#11474=DIRECTION('',(0.,0.,1.));
#11475=DIRECTION('center_axis',(0.,0.,-1.));
#11476=DIRECTION('ref_axis',(1.,0.,0.));
#11477=DIRECTION('center_axis',(0.,0.,1.));
#11478=DIRECTION('ref_axis',(1.,0.,0.));
#11479=DIRECTION('',(0.,0.,1.));
#11480=DIRECTION('center_axis',(0.,0.,1.));
#11481=DIRECTION('ref_axis',(1.,0.,0.));
#11482=DIRECTION('',(0.,0.,1.));
#11483=DIRECTION('center_axis',(0.,0.,1.));
#11484=DIRECTION('ref_axis',(0.936891279057678,0.349620839232545,0.));
#11485=DIRECTION('',(0.,0.,1.));
#11486=DIRECTION('center_axis',(0.,0.,-1.));
#11487=DIRECTION('ref_axis',(1.,0.,0.));
#11488=DIRECTION('center_axis',(0.,0.,1.));
#11489=DIRECTION('ref_axis',(1.,-1.48847114380753E-15,0.));
#11490=DIRECTION('',(1.22464679914735E-16,-1.6728754436209E-31,1.));
#11491=DIRECTION('center_axis',(0.,0.,-1.));
#11492=DIRECTION('ref_axis',(1.,-1.48847114380753E-15,0.));
#11493=DIRECTION('center_axis',(0.,0.,1.));
#11494=DIRECTION('ref_axis',(1.,-1.48847114380753E-15,0.));
#11495=DIRECTION('',(1.22464679914735E-16,-1.6728754436209E-31,1.));
#11496=DIRECTION('center_axis',(0.,0.,1.));
#11497=DIRECTION('ref_axis',(1.,-1.48847114380753E-15,0.));
#11498=DIRECTION('',(1.22464679914735E-16,-1.6728754436209E-31,1.));
#11499=DIRECTION('center_axis',(0.,0.,1.));
#11500=DIRECTION('ref_axis',(-0.608867914098284,0.793271620053059,0.));
#11501=DIRECTION('',(1.22464679914735E-16,-1.6728754436209E-31,1.));
#11502=DIRECTION('center_axis',(0.,0.,1.));
#11503=DIRECTION('ref_axis',(1.,-1.48847114380753E-15,0.));
#11504=DIRECTION('center_axis',(0.,0.,1.));
#11505=DIRECTION('ref_axis',(1.,-1.48847114380753E-15,0.));
#11506=DIRECTION('center_axis',(0.,0.,1.));
#11507=DIRECTION('ref_axis',(1.,0.,0.));
#11508=DIRECTION('',(0.5,0.866025403784439,0.));
#11509=DIRECTION('',(-0.5,0.866025403784439,0.));
#11510=DIRECTION('',(-1.,0.,0.));
#11511=DIRECTION('',(-0.5,-0.866025403784439,0.));
#11512=DIRECTION('',(0.499999999999999,-0.866025403784439,0.));
#11513=DIRECTION('',(1.,-2.13662520709285E-16,0.));
#11514=DIRECTION('center_axis',(0.,0.,1.));
#11515=DIRECTION('ref_axis',(1.,0.,0.));
#11516=DIRECTION('center_axis',(-2.13662520709285E-16,-1.,0.));
#11517=DIRECTION('ref_axis',(1.,-2.13662520709285E-16,0.));
#11518=DIRECTION('',(1.,-2.13662520709285E-16,0.));
#11519=DIRECTION('',(0.,0.,1.));
#11520=DIRECTION('',(0.,0.,1.));
#11521=DIRECTION('center_axis',(-0.866025403784439,-0.499999999999999,0.));
#11522=DIRECTION('ref_axis',(0.499999999999999,-0.866025403784439,0.));
#11523=DIRECTION('',(0.499999999999999,-0.866025403784439,0.));
#11524=DIRECTION('',(0.,0.,1.));
#11525=DIRECTION('center_axis',(-0.866025403784439,0.5,0.));
#11526=DIRECTION('ref_axis',(-0.5,-0.866025403784439,0.));
#11527=DIRECTION('',(-0.5,-0.866025403784439,0.));
#11528=DIRECTION('',(0.,0.,1.));
#11529=DIRECTION('center_axis',(0.,1.,0.));
#11530=DIRECTION('ref_axis',(-1.,0.,0.));
#11531=DIRECTION('',(-1.,0.,0.));
#11532=DIRECTION('',(0.,0.,1.));
#11533=DIRECTION('center_axis',(0.866025403784439,0.5,0.));
#11534=DIRECTION('ref_axis',(-0.5,0.866025403784439,0.));
#11535=DIRECTION('',(-0.5,0.866025403784439,0.));
#11536=DIRECTION('',(0.,0.,1.));
#11537=DIRECTION('center_axis',(0.866025403784439,-0.5,0.));
#11538=DIRECTION('ref_axis',(0.5,0.866025403784439,0.));
#11539=DIRECTION('',(0.5,0.866025403784439,0.));
#11540=DIRECTION('center_axis',(0.,0.,1.));
#11541=DIRECTION('ref_axis',(1.,0.,0.));
#30301=CARTESIAN_POINT('',(0.,0.,0.));
#30302=CARTESIAN_POINT('Origin',(-8.5,0.,16.1));
#30303=CARTESIAN_POINT('',(-9.55012800649379,-2.18440497826711E-5,17.2841069671524));
#30304=CARTESIAN_POINT('',(-9.5500106216945,-1.13051919086155E-6,17.3658930328476));
#30305=CARTESIAN_POINT('',(-9.5501,-1.28600160378464E-16,16.1));
#30306=CARTESIAN_POINT('',(-9.29338130674014,-0.687936125025652,17.4));
#30307=CARTESIAN_POINT('Ctrl Pts',(-9.5500106216945,-1.13051919086155E-6,
17.3658930328476));
#30308=CARTESIAN_POINT('Ctrl Pts',(-9.55001831318254,-0.0803156021754179,
17.3695440482821));
#30309=CARTESIAN_POINT('Ctrl Pts',(-9.5409068063874,-0.160625002221925,
17.3731950637165));
#30310=CARTESIAN_POINT('Ctrl Pts',(-9.52264867059269,-0.238791324198228,
17.3768460791509));
#30311=CARTESIAN_POINT('Ctrl Pts',(-9.48405233681149,-0.404029083812233,
17.3845640527673));
#30312=CARTESIAN_POINT('Ctrl Pts',(-9.40458264633922,-0.55969011364039,
17.3922820263836));
#30313=CARTESIAN_POINT('Ctrl Pts',(-9.29338130674014,-0.687936125025652,
17.4));
#30314=CARTESIAN_POINT('',(-7.70661869325993,-0.687936125025728,17.4));
#30315=CARTESIAN_POINT('Origin',(-8.5,0.,17.4));
#30316=CARTESIAN_POINT('Ctrl Pts',(-7.70658083841847,-0.687941007616013,
17.4));
#30317=CARTESIAN_POINT('Ctrl Pts',(-7.79864150585798,-0.793915583878177,
17.3936166544345));
#30318=CARTESIAN_POINT('Ctrl Pts',(-7.91206827104569,-0.881430774697101,
17.387233308869));
#30319=CARTESIAN_POINT('Ctrl Pts',(-8.03812217198675,-0.943160594462135,
17.3808499633034));
#30320=CARTESIAN_POINT('Ctrl Pts',(-8.19053138620163,-1.01779686715008,
17.3731319896871));
#30321=CARTESIAN_POINT('Ctrl Pts',(-8.36139987870404,-1.05473818277663,
17.3654140160707));
#30322=CARTESIAN_POINT('Ctrl Pts',(-8.5310286260214,-1.04972425335905,17.3576960424544));
#30323=CARTESIAN_POINT('Ctrl Pts',(-8.70065737333876,-1.04471032394146,
17.349978068838));
#30324=CARTESIAN_POINT('Ctrl Pts',(-8.86904637547108,-0.99774114947973,
17.3422600952216));
#30325=CARTESIAN_POINT('Ctrl Pts',(-9.016780747997,-0.914232530587763,17.3345421216053));
#30326=CARTESIAN_POINT('Ctrl Pts',(-9.16451512052293,-0.830723911695799,
17.3268241479889));
#30327=CARTESIAN_POINT('Ctrl Pts',(-9.29159486344247,-0.7106758483736,17.3191061743725));
#30328=CARTESIAN_POINT('Ctrl Pts',(-9.38336862586148,-0.567928987999592,
17.3113882007562));
#30329=CARTESIAN_POINT('Ctrl Pts',(-9.47514238828048,-0.425182127625583,
17.3036702271398));
#30330=CARTESIAN_POINT('Ctrl Pts',(-9.53161017019895,-0.259736470199762,
17.2959522535235));
#30331=CARTESIAN_POINT('Ctrl Pts',(-9.5462614276818,-0.0906671084845678,
17.2882342799071));
#30332=CARTESIAN_POINT('Ctrl Pts',(-9.5488730942879,-0.0605295720566002,
17.2868585089888));
#30333=CARTESIAN_POINT('Ctrl Pts',(-9.5501560404896,-0.0302768923953349,
17.2854827380706));
#30334=CARTESIAN_POINT('Ctrl Pts',(-9.55012800649379,-2.18440497826711E-5,
17.2841069671524));
#30335=CARTESIAN_POINT('Origin',(-8.5,0.,16.1));
#30336=CARTESIAN_POINT('',(-9.55014795915375,-1.85392213186142E-5,16.9841069671524));
#30337=CARTESIAN_POINT('',(-9.55002861856303,-9.63118433582547E-6,17.0658930328476));
#30338=CARTESIAN_POINT('',(-9.5501,-1.28600160378464E-16,16.1));
#30339=CARTESIAN_POINT('Ctrl Pts',(-9.55002861856303,-9.63118433582547E-6,
17.0658930328476));
#30340=CARTESIAN_POINT('Ctrl Pts',(-9.5500534563119,-0.0729826763478919,
17.0692103912693));
#30341=CARTESIAN_POINT('Ctrl Pts',(-9.54254615138756,-0.145950682283606,
17.0725277496911));
#30342=CARTESIAN_POINT('Ctrl Pts',(-9.5274522464353,-0.217314064080866,
17.0758451081128));
#30343=CARTESIAN_POINT('Ctrl Pts',(-9.49233564298756,-0.38334396735565,
17.0835630817291));
#30344=CARTESIAN_POINT('Ctrl Pts',(-9.41615430938654,-0.540688365002029,
17.0912810553455));
#30345=CARTESIAN_POINT('Ctrl Pts',(-9.30769153933757,-0.6712063014371,17.0989990289619));
#30346=CARTESIAN_POINT('Ctrl Pts',(-9.1992287692886,-0.801724237872172,
17.1067170025782));
#30347=CARTESIAN_POINT('Ctrl Pts',(-9.05848456279167,-0.905415713095935,
17.1144349761946));
#30348=CARTESIAN_POINT('Ctrl Pts',(-8.90168595900391,-0.970325671537641,
17.122152949811));
#30349=CARTESIAN_POINT('Ctrl Pts',(-8.74488735521615,-1.03523562997935,
17.1298709234273));
#30350=CARTESIAN_POINT('Ctrl Pts',(-8.57203435413756,-1.061364071639,17.1375888970437));
#30351=CARTESIAN_POINT('Ctrl Pts',(-8.40305596905745,-1.04569851429791,
17.14530687066));
#30352=CARTESIAN_POINT('Ctrl Pts',(-8.23407758397734,-1.03003295695682,
17.1530248442764));
#30353=CARTESIAN_POINT('Ctrl Pts',(-8.06897381489572,-0.972573400614992,
17.1607428178928));
#30354=CARTESIAN_POINT('Ctrl Pts',(-7.92678022008012,-0.879944652158432,
17.1684607915091));
#30355=CARTESIAN_POINT('Ctrl Pts',(-7.78458662526451,-0.787315903701873,
17.1761787651255));
#30356=CARTESIAN_POINT('Ctrl Pts',(-7.66530320471492,-0.659517963130584,
17.1838967387419));
#30357=CARTESIAN_POINT('Ctrl Pts',(-7.58268270323884,-0.511285165544643,
17.1916147123582));
#30358=CARTESIAN_POINT('Ctrl Pts',(-7.50006220176276,-0.363052367958701,
17.1993326859746));
#30359=CARTESIAN_POINT('Ctrl Pts',(-7.45410461936019,-0.194384713358108,
17.2070506595909));
#30360=CARTESIAN_POINT('Ctrl Pts',(-7.45010857988296,-0.0247288190203272,
17.2147686332073));
#30361=CARTESIAN_POINT('Ctrl Pts',(-7.44611254040573,0.144927075317456,
17.2224866068237));
#30362=CARTESIAN_POINT('Ctrl Pts',(-7.48407804385384,0.315571209392425,
17.23020458044));
#30363=CARTESIAN_POINT('Ctrl Pts',(-7.55962794825812,0.467529582998103,
17.2379225540564));
#30364=CARTESIAN_POINT('Ctrl Pts',(-7.6351778526624,0.619487956603781,17.2456405276728));
#30365=CARTESIAN_POINT('Ctrl Pts',(-7.74831215802285,0.752760569740168,
17.2533585012891));
#30366=CARTESIAN_POINT('Ctrl Pts',(-7.88598692485404,0.851981087282268,
17.2610764749055));
#30367=CARTESIAN_POINT('Ctrl Pts',(-8.02366169168523,0.951201604824368,
17.2687944485218));
#30368=CARTESIAN_POINT('Ctrl Pts',(-8.18587691998715,1.01637002677218,17.2765124221382));
#30369=CARTESIAN_POINT('Ctrl Pts',(-8.35393041166614,1.03997440538661,17.2842303957546));
#30370=CARTESIAN_POINT('Ctrl Pts',(-8.52198390334514,1.06357878400103,17.2919483693709));
#30371=CARTESIAN_POINT('Ctrl Pts',(-8.6958756584012,1.04561911928206,17.2996663429873));
#30372=CARTESIAN_POINT('Ctrl Pts',(-8.85555604832858,0.988162672768926,
17.3073843166036));
#30373=CARTESIAN_POINT('Ctrl Pts',(-9.01523643825595,0.930706226255792,
17.31510229022));
#30374=CARTESIAN_POINT('Ctrl Pts',(-9.16070546305465,0.833752997948491,
17.3228202638364));
#30375=CARTESIAN_POINT('Ctrl Pts',(-9.2751927205708,0.708488991223898,17.3305382374527));
#30376=CARTESIAN_POINT('Ctrl Pts',(-9.38967997808695,0.5832249844993,17.3382562110691));
#30377=CARTESIAN_POINT('Ctrl Pts',(-9.47318546832054,0.429650199357407,
17.3459741846855));
#30378=CARTESIAN_POINT('Ctrl Pts',(-9.51607672489228,0.265455562086529,
17.3536921583018));
#30379=CARTESIAN_POINT('Ctrl Pts',(-9.53867811685325,0.178933793981138,
17.3577591164838));
#30380=CARTESIAN_POINT('Ctrl Pts',(-9.55000205395197,0.0894631852297447,
17.3618260746657));
#30381=CARTESIAN_POINT('Ctrl Pts',(-9.5500106216945,-1.13051919086155E-6,
17.3658930328476));
#30382=CARTESIAN_POINT('Ctrl Pts',(-9.55012800649379,-2.18440497826711E-5,
17.2841069671524));
#30383=CARTESIAN_POINT('Ctrl Pts',(-9.54999877183601,0.139451702530489,
17.2777647644542));
#30384=CARTESIAN_POINT('Ctrl Pts',(-9.52200934434521,0.278975587019088,
17.2714225617561));
#30385=CARTESIAN_POINT('Ctrl Pts',(-9.46789768755617,0.407501569956399,
17.265080359058));
#30386=CARTESIAN_POINT('Ctrl Pts',(-9.40204795690043,0.563907820677612,
17.2573623854416));
#30387=CARTESIAN_POINT('Ctrl Pts',(-9.29751376254171,0.704027256115468,
17.2496444118253));
#30388=CARTESIAN_POINT('Ctrl Pts',(-9.16634730336329,0.811704845033145,
17.2419264382089));
#30389=CARTESIAN_POINT('Ctrl Pts',(-9.03518084418487,0.919382433950822,
17.2342084645926));
#30390=CARTESIAN_POINT('Ctrl Pts',(-8.87738212018675,0.994618176348321,
17.2264904909762));
#30391=CARTESIAN_POINT('Ctrl Pts',(-8.7111444764068,1.02873781147201,17.2187725173598));
#30392=CARTESIAN_POINT('Ctrl Pts',(-8.54490683262685,1.0628574465957,17.2110545437435));
#30393=CARTESIAN_POINT('Ctrl Pts',(-8.37023026906508,1.05586097444558,17.2033365701271));
#30394=CARTESIAN_POINT('Ctrl Pts',(-8.20725403725456,1.00855504524276,17.1956185965107));
#30395=CARTESIAN_POINT('Ctrl Pts',(-8.04427780544405,0.961249116039934,
17.1879006228944));
#30396=CARTESIAN_POINT('Ctrl Pts',(-7.8930019053848,0.873633729784408,17.180182649278));
#30397=CARTESIAN_POINT('Ctrl Pts',(-7.77086762711664,0.755810465752038,
17.1724646756617));
#30398=CARTESIAN_POINT('Ctrl Pts',(-7.64873334884848,0.637987201719667,
17.1647467020453));
#30399=CARTESIAN_POINT('Ctrl Pts',(-7.55574069237142,0.489956059910451,
17.1570287284289));
#30400=CARTESIAN_POINT('Ctrl Pts',(-7.50261120356912,0.328784223964852,
17.1493107548126));
#30401=CARTESIAN_POINT('Ctrl Pts',(-7.44948171476683,0.167612388019253,
17.1415927811962));
#30402=CARTESIAN_POINT('Ctrl Pts',(-7.4362153936393,-0.00670014206272976,
17.1338748075798));
#30403=CARTESIAN_POINT('Ctrl Pts',(-7.46434177529062,-0.17405608013945,
17.1261568339635));
#30404=CARTESIAN_POINT('Ctrl Pts',(-7.49246815694194,-0.341412018216172,
17.1184388603471));
#30405=CARTESIAN_POINT('Ctrl Pts',(-7.56198724137211,-0.501811364287633,
17.1107208867308));
#30406=CARTESIAN_POINT('Ctrl Pts',(-7.66488385641448,-0.636760947278931,
17.1030029131144));
#30407=CARTESIAN_POINT('Ctrl Pts',(-7.76778047145686,-0.771710530270227,
17.095284939498));
#30408=CARTESIAN_POINT('Ctrl Pts',(-7.90405461711142,-0.881210350181365,
17.0875669658817));
#30409=CARTESIAN_POINT('Ctrl Pts',(-8.05799462644632,-0.952635673854597,
17.0798489922653));
#30410=CARTESIAN_POINT('Ctrl Pts',(-8.21193463578122,-1.02406099752783,
17.0721310186489));
#30411=CARTESIAN_POINT('Ctrl Pts',(-8.38354050879644,-1.05741182496316,
17.0644130450326));
#30412=CARTESIAN_POINT('Ctrl Pts',(-8.5530270226046,-1.04884298738516,17.0566950714162));
#30413=CARTESIAN_POINT('Ctrl Pts',(-8.72251353641277,-1.04027414980716,
17.0489770977999));
#30414=CARTESIAN_POINT('Ctrl Pts',(-8.88988069101389,-0.989785647215842,
17.0412591241835));
#30415=CARTESIAN_POINT('Ctrl Pts',(-9.03583196474797,-0.903198529050057,
17.0335411505671));
#30416=CARTESIAN_POINT('Ctrl Pts',(-9.18178323848206,-0.816611410884273,
17.0258231769508));
#30417=CARTESIAN_POINT('Ctrl Pts',(-9.3063186313491,-0.693925677144025,
17.0181052033344));
#30418=CARTESIAN_POINT('Ctrl Pts',(-9.39507989058315,-0.549286324968012,
17.010387229718));
#30419=CARTESIAN_POINT('Ctrl Pts',(-9.48384114981719,-0.404646972791997,
17.0026692561017));
#30420=CARTESIAN_POINT('Ctrl Pts',(-9.53682827541823,-0.238054002180217,
16.9949512824853));
#30421=CARTESIAN_POINT('Ctrl Pts',(-9.54793214030158,-0.0687146756119928,
16.987233308869));
#30422=CARTESIAN_POINT('Ctrl Pts',(-9.54943143177046,-0.0458497533225895,
16.9861911949634));
#30423=CARTESIAN_POINT('Ctrl Pts',(-9.55016712610837,-0.0229347606830505,
16.9851490810579));
#30424=CARTESIAN_POINT('Ctrl Pts',(-9.55014795915375,-1.85392213186142E-5,
16.9841069671524));
#30425=CARTESIAN_POINT('Origin',(-8.5,0.,16.1));
#30426=CARTESIAN_POINT('',(-9.55016499124735,-1.36965953006496E-5,16.6841069671524));
#30427=CARTESIAN_POINT('',(-9.55003851802847,-1.48519297202892E-5,16.7658930328476));
#30428=CARTESIAN_POINT('',(-9.5501,-1.28600160378464E-16,16.1));
#30429=CARTESIAN_POINT('Ctrl Pts',(-9.55003851802847,-1.48519297202892E-5,
16.7658930328476));
#30430=CARTESIAN_POINT('Ctrl Pts',(-9.55007343104712,-0.065646556384278,
16.7688767342566));
#30431=CARTESIAN_POINT('Ctrl Pts',(-9.54400925298908,-0.131271887510206,
16.7718604356656));
#30432=CARTESIAN_POINT('Ctrl Pts',(-9.53178197230159,-0.195728083779944,
16.7748441370746));
#30433=CARTESIAN_POINT('Ctrl Pts',(-9.50015352936794,-0.362457643486915,
16.782562110691));
#30434=CARTESIAN_POINT('Ctrl Pts',(-9.42728730806163,-0.521364434860128,
16.7902800843074));
#30435=CARTESIAN_POINT('Ctrl Pts',(-9.32158438697376,-0.654127370034059,
16.7979980579237));
#30436=CARTESIAN_POINT('Ctrl Pts',(-9.21588146588589,-0.786890305207989,
16.8057160315401));
#30437=CARTESIAN_POINT('Ctrl Pts',(-9.07734184501646,-0.893509384182638,
16.8134340051565));
#30438=CARTESIAN_POINT('Ctrl Pts',(-8.92193838836266,-0.961692007647338,
16.8211519787728));
#30439=CARTESIAN_POINT('Ctrl Pts',(-8.76653493170886,-1.02987463111204,
16.8288699523892));
#30440=CARTESIAN_POINT('Ctrl Pts',(-8.59426763927069,-1.05962079906679,
16.8365879260055));
#30441=CARTESIAN_POINT('Ctrl Pts',(-8.42499799194421,-1.04750094030223,
16.8443058996219));
#30442=CARTESIAN_POINT('Ctrl Pts',(-8.25572834461773,-1.03538108153767,
16.8520238732383));
#30443=CARTESIAN_POINT('Ctrl Pts',(-8.08945634240295,-0.9813951960538,16.8597418468546));
#30444=CARTESIAN_POINT('Ctrl Pts',(-7.94535224187542,-0.89176756251543,
16.867459820471));
#30445=CARTESIAN_POINT('Ctrl Pts',(-7.8012481413479,-0.802139928977061,
16.8751777940874));
#30446=CARTESIAN_POINT('Ctrl Pts',(-7.67931194250762,-0.676870547384194,
16.8828957677037));
#30447=CARTESIAN_POINT('Ctrl Pts',(-7.59360222518964,-0.530402295399115,
16.8906137413201));
#30448=CARTESIAN_POINT('Ctrl Pts',(-7.50789250787166,-0.383934043414033,
16.8983317149364));
#30449=CARTESIAN_POINT('Ctrl Pts',(-7.45840927207598,-0.216266921036739,
16.9060496885528));
#30450=CARTESIAN_POINT('Ctrl Pts',(-7.45085766547616,-0.0467320345949428,
16.9137676621692));
#30451=CARTESIAN_POINT('Ctrl Pts',(-7.44330605887635,0.122802851846853,
16.9214856357855));
#30452=CARTESIAN_POINT('Ctrl Pts',(-7.4776860814724,0.294205502353147,16.9292036094019));
#30453=CARTESIAN_POINT('Ctrl Pts',(-7.55003390384043,0.447714124520869,
16.9369215830182));
#30454=CARTESIAN_POINT('Ctrl Pts',(-7.62238172620845,0.60122274668859,16.9446395566346));
#30455=CARTESIAN_POINT('Ctrl Pts',(-7.73269734834845,0.736837340517737,
16.952357530251));
#30456=CARTESIAN_POINT('Ctrl Pts',(-7.86826197965597,0.838922281733849,
16.9600755038673));
#30457=CARTESIAN_POINT('Ctrl Pts',(-8.0038266109635,0.941007222949962,16.9677934774837));
#30458=CARTESIAN_POINT('Ctrl Pts',(-8.16464025143855,1.00956251155304,16.9755114511001));
#30459=CARTESIAN_POINT('Ctrl Pts',(-8.33216196388124,1.0366840959553,16.9832294247164));
#30460=CARTESIAN_POINT('Ctrl Pts',(-8.49968367632392,1.06380568035755,16.9909473983328));
#30461=CARTESIAN_POINT('Ctrl Pts',(-8.67391346073423,1.04949356055899,16.9986653719492));
#30462=CARTESIAN_POINT('Ctrl Pts',(-8.83476357160864,0.995397846192756,
17.0063833455655));
#30463=CARTESIAN_POINT('Ctrl Pts',(-8.99561368248304,0.941302131826525,
17.0141013191819));
#30464=CARTESIAN_POINT('Ctrl Pts',(-9.14308411982153,0.84742282289263,17.0218192927982));
#30465=CARTESIAN_POINT('Ctrl Pts',(-9.26017234504276,0.724583692265943,
17.0295372664146));
#30466=CARTESIAN_POINT('Ctrl Pts',(-9.37726057026399,0.601744561639255,
17.037255240031));
#30467=CARTESIAN_POINT('Ctrl Pts',(-9.46396658336796,0.449945609319775,
17.0449732136473));
#30468=CARTESIAN_POINT('Ctrl Pts',(-9.51029365327272,0.286688428708442,
17.0526911872637));
#30469=CARTESIAN_POINT('Ctrl Pts',(-9.53670830793207,0.193602851412619,
17.0570918024583));
#30470=CARTESIAN_POINT('Ctrl Pts',(-9.54999567024658,0.0967921763152249,
17.061492417653));
#30471=CARTESIAN_POINT('Ctrl Pts',(-9.55002861856303,-9.63118433582547E-6,
17.0658930328476));
#30472=CARTESIAN_POINT('Ctrl Pts',(-9.55014795915375,-1.85392213186142E-5,
16.9841069671524));
#30473=CARTESIAN_POINT('Ctrl Pts',(-9.55002517420727,0.146784491396649,
16.9774311074415));
#30474=CARTESIAN_POINT('Ctrl Pts',(-9.51892454602037,0.293637950168291,
16.9707552477307));
#30475=CARTESIAN_POINT('Ctrl Pts',(-9.45914264955535,0.427701829697936,
16.9640793880199));
#30476=CARTESIAN_POINT('Ctrl Pts',(-9.39002868976012,0.58269332591497,16.9563614144035));
#30477=CARTESIAN_POINT('Ctrl Pts',(-9.28258016600401,0.720590635824375,
16.9486434407871));
#30478=CARTESIAN_POINT('Ctrl Pts',(-9.14918530806574,0.82549495038658,16.9409254671708));
#30479=CARTESIAN_POINT('Ctrl Pts',(-9.01579045012747,0.930399264948787,
16.9332074935544));
#30480=CARTESIAN_POINT('Ctrl Pts',(-8.85644925800704,1.00231058416379,16.9254895199381));
#30481=CARTESIAN_POINT('Ctrl Pts',(-8.68953290361066,1.03293792445212,16.9177715463217));
#30482=CARTESIAN_POINT('Ctrl Pts',(-8.52261654921428,1.06356526474045,16.9100535727053));
#30483=CARTESIAN_POINT('Ctrl Pts',(-8.34812503254195,1.05290862610209,16.902335599089));
#30484=CARTESIAN_POINT('Ctrl Pts',(-8.18617627543435,1.00219666095141,16.8946176254726));
#30485=CARTESIAN_POINT('Ctrl Pts',(-8.02422751832675,0.951484695800729,
16.8868996518562));
#30486=CARTESIAN_POINT('Ctrl Pts',(-7.87482152078387,0.860717404137714,
16.8791816782399));
#30487=CARTESIAN_POINT('Ctrl Pts',(-7.7551839808704,0.740359760501857,16.8714637046235));
#30488=CARTESIAN_POINT('Ctrl Pts',(-7.63554644095693,0.620002116866001,
16.8637457310072));
#30489=CARTESIAN_POINT('Ctrl Pts',(-7.54567735867286,0.470054121257305,
16.8560277573908));
#30490=CARTESIAN_POINT('Ctrl Pts',(-7.49593814990679,0.3078039611666,16.8483097837744));
#30491=CARTESIAN_POINT('Ctrl Pts',(-7.44619894114072,0.145553801075895,
16.8405918101581));
#30492=CARTESIAN_POINT('Ctrl Pts',(-7.43658960589264,-0.0289985234968166,
16.8328738365417));
#30493=CARTESIAN_POINT('Ctrl Pts',(-7.4682180481979,-0.195728079891194,
16.8251558629253));
#30494=CARTESIAN_POINT('Ctrl Pts',(-7.49984649050317,-0.362457636285574,
16.817437889309));
#30495=CARTESIAN_POINT('Ctrl Pts',(-7.57271271036177,-0.521364424501619,
16.8097199156926));
#30496=CARTESIAN_POINT('Ctrl Pts',(-7.67841562934952,-0.65412735703781,
16.8020019420763));
#30497=CARTESIAN_POINT('Ctrl Pts',(-7.78411854833728,-0.786890289574002,
16.7942839684599));
#30498=CARTESIAN_POINT('Ctrl Pts',(-7.92265816645419,-0.893509366430338,
16.7865659948435));
#30499=CARTESIAN_POINT('Ctrl Pts',(-8.07806162002042,-0.961691988540383,
16.7788480212272));
#30500=CARTESIAN_POINT('Ctrl Pts',(-8.23346507358666,-1.02987461065043,
16.7711300476108));
#30501=CARTESIAN_POINT('Ctrl Pts',(-8.40573236260221,-1.05962077801418,
16.7634120739944));
#30502=CARTESIAN_POINT('Ctrl Pts',(-8.57500200656563,-1.04750091949042,
16.7556941003781));
#30503=CARTESIAN_POINT('Ctrl Pts',(-8.74427165052905,-1.03538106096666,
16.7479761267617));
#30504=CARTESIAN_POINT('Ctrl Pts',(-8.91054364944032,-0.981395176555395,
16.7402581531454));
#30505=CARTESIAN_POINT('Ctrl Pts',(-9.05464774710478,-0.891767544797753,
16.732540179529));
#30506=CARTESIAN_POINT('Ctrl Pts',(-9.19875184476925,-0.80213991304011,
16.7248222059126));
#30507=CARTESIAN_POINT('Ctrl Pts',(-9.32068804118689,-0.676870533936093,
16.7171042322963));
#30508=CARTESIAN_POINT('Ctrl Pts',(-9.40639775680199,-0.530402284861058,
16.7093862586799));
#30509=CARTESIAN_POINT('Ctrl Pts',(-9.49210747241709,-0.383934035786023,
16.7016682850636));
#30510=CARTESIAN_POINT('Ctrl Pts',(-9.54159070722963,-0.216266916739969,
16.6939503114472));
#30511=CARTESIAN_POINT('Ctrl Pts',(-9.54914231367942,-0.0467320336664906,
16.6862323378308));
#30512=CARTESIAN_POINT('Ctrl Pts',(-9.54983549921064,-0.0311698974819526,
16.685523880938));
#30513=CARTESIAN_POINT('Ctrl Pts',(-9.5501753697963,-0.0155920235602596,
16.6848154240452));
#30514=CARTESIAN_POINT('Ctrl Pts',(-9.55016499124735,-1.36965953006496E-5,
16.6841069671524));
#30515=CARTESIAN_POINT('Origin',(-8.5,0.,16.1));
#30516=CARTESIAN_POINT('',(-9.55017719779692,-7.61530804432864E-6,16.3841069671524));
#30517=CARTESIAN_POINT('',(-9.55005247215833,-1.9100347204657E-5,16.4658930328476));
#30518=CARTESIAN_POINT('',(-9.5501,-1.28600160378464E-16,16.1));
#30519=CARTESIAN_POINT('',(-7.70661869325986,-0.687936125025652,16.2));
#30520=CARTESIAN_POINT('Ctrl Pts',(-9.55017719779692,-7.61530804432864E-6,
16.3841069671524));
#30521=CARTESIAN_POINT('Ctrl Pts',(-9.55011144655369,0.161456631165944,
16.3767637934161));
#30522=CARTESIAN_POINT('Ctrl Pts',(-9.51225308460155,0.322950597851874,
16.3694206196799));
#30523=CARTESIAN_POINT('Ctrl Pts',(-9.44037203261531,0.467529573139717,
16.3620774459436));
#30524=CARTESIAN_POINT('Ctrl Pts',(-9.36482212971608,0.619487943842984,
16.3543594723272));
#30525=CARTESIAN_POINT('Ctrl Pts',(-9.25168782689266,0.75276055510798,16.3466414987109));
#30526=CARTESIAN_POINT('Ctrl Pts',(-9.11401306207929,0.851981069812583,
16.3389235250945));
#30527=CARTESIAN_POINT('Ctrl Pts',(-8.97633829726593,0.951201584517186,
16.3312055514782));
#30528=CARTESIAN_POINT('Ctrl Pts',(-8.81412307046263,1.01637000266139,16.3234875778618));
#30529=CARTESIAN_POINT('Ctrl Pts',(-8.64606958159429,1.03997438059275,16.3157696042454));
#30530=CARTESIAN_POINT('Ctrl Pts',(-8.47801609272595,1.06357875852411,16.3080516306291));
#30531=CARTESIAN_POINT('Ctrl Pts',(-8.30412434179258,1.04561909624262,16.3003336570127));
#30532=CARTESIAN_POINT('Ctrl Pts',(-8.14444395006926,0.988162645854508,
16.2926156833963));
#30533=CARTESIAN_POINT('Ctrl Pts',(-7.98476355834595,0.930706195466399,
16.28489770978));
#30534=CARTESIAN_POINT('Ctrl Pts',(-7.8392945258327,0.833752956971675,16.2771797361636));
#30535=CARTESIAN_POINT('Ctrl Pts',(-7.72480726549775,0.708488948192354,
16.2694617625473));
#30536=CARTESIAN_POINT('Ctrl Pts',(-7.6103200051628,0.583224939413033,16.2617437889309));
#30537=CARTESIAN_POINT('Ctrl Pts',(-7.52681451700616,0.429650160349115,
16.2540258153145));
#30538=CARTESIAN_POINT('Ctrl Pts',(-7.48392323634831,0.26545550415572,16.2463078416982));
#30539=CARTESIAN_POINT('Ctrl Pts',(-7.44103195569046,0.101260847962323,
16.2385898680818));
#30540=CARTESIAN_POINT('Ctrl Pts',(-7.4387548825314,-0.0735536853605511,
16.2308718944654));
#30541=CARTESIAN_POINT('Ctrl Pts',(-7.47735123202398,-0.23879142576123,
16.2231539208491));
#30542=CARTESIAN_POINT('Ctrl Pts',(-7.51594758151656,-0.404029166161908,
16.2154359472327));
#30543=CARTESIAN_POINT('Ctrl Pts',(-7.59541735366078,-0.559690113640392,
16.2077179736164));
#30544=CARTESIAN_POINT('Ctrl Pts',(-7.70661869325987,-0.687936125025659,
16.2));
#30545=CARTESIAN_POINT('',(-9.293419174865,-0.687941029322388,16.2));
#30546=CARTESIAN_POINT('Origin',(-8.5,0.,16.2));
#30547=CARTESIAN_POINT('Ctrl Pts',(-9.293419174865,-0.687941029322388,16.2));
#30548=CARTESIAN_POINT('Ctrl Pts',(-9.20135850648669,-0.793915604248618,
16.2063833455655));
#30549=CARTESIAN_POINT('Ctrl Pts',(-9.08793173951017,-0.881430798173356,
16.212766691131));
#30550=CARTESIAN_POINT('Ctrl Pts',(-8.96187783632725,-0.943160618773336,
16.2191500366966));
#30551=CARTESIAN_POINT('Ctrl Pts',(-8.80946861940179,-1.01779689247079,
16.2268680103129));
#30552=CARTESIAN_POINT('Ctrl Pts',(-8.63860012352652,-1.05473820578714,
16.2345859839293));
#30553=CARTESIAN_POINT('Ctrl Pts',(-8.46897137294775,-1.04972427515045,
16.2423039575456));
#30554=CARTESIAN_POINT('Ctrl Pts',(-8.29934262236897,-1.04471034451375,
16.250021931162));
#30555=CARTESIAN_POINT('Ctrl Pts',(-8.1309536170867,-0.997741169924025,
16.2577399047784));
#30556=CARTESIAN_POINT('Ctrl Pts',(-7.98321924168765,-0.914232549471815,
16.2654578783947));
#30557=CARTESIAN_POINT('Ctrl Pts',(-7.8354848662886,-0.830723929019605,
16.2731758520111));
#30558=CARTESIAN_POINT('Ctrl Pts',(-7.70840512077277,-0.710675862704915,
16.2808938256275));
#30559=CARTESIAN_POINT('Ctrl Pts',(-7.61663135652483,-0.56792899930393,
16.2886117992438));
#30560=CARTESIAN_POINT('Ctrl Pts',(-7.52485759227689,-0.425182135902946,
16.2963297728602));
#30561=CARTESIAN_POINT('Ctrl Pts',(-7.46838980929684,-0.259736475415666,
16.3040477464765));
#30562=CARTESIAN_POINT('Ctrl Pts',(-7.45373855153845,-0.0906671103893211,
16.3117657200929));
#30563=CARTESIAN_POINT('Ctrl Pts',(-7.43908729378006,0.0784022546370248,
16.3194836937093));
#30564=CARTESIAN_POINT('Ctrl Pts',(-7.46625256124332,0.251095324202436,
16.3272016673256));
#30565=CARTESIAN_POINT('Ctrl Pts',(-7.53210229320152,0.407501578067959,
16.334919640942));
#30566=CARTESIAN_POINT('Ctrl Pts',(-7.59795202515973,0.56390783193348,16.3426376145583));
#30567=CARTESIAN_POINT('Ctrl Pts',(-7.70248622161286,0.704027270099115,
16.3503555881747));
#30568=CARTESIAN_POINT('Ctrl Pts',(-7.83365268340161,0.811704861142506,
16.3580735617911));
#30569=CARTESIAN_POINT('Ctrl Pts',(-7.96481914519036,0.919382452185898,
16.3657915354074));
#30570=CARTESIAN_POINT('Ctrl Pts',(-8.12261787231473,0.994618196107047,
16.3735095090238));
#30571=CARTESIAN_POINT('Ctrl Pts',(-8.28885551939544,1.02873783191642,16.3812274826402));
#30572=CARTESIAN_POINT('Ctrl Pts',(-8.45509316647615,1.06285746772579,16.3889454562565));
#30573=CARTESIAN_POINT('Ctrl Pts',(-8.6297697335132,1.05586099542339,16.3966634298729));
#30574=CARTESIAN_POINT('Ctrl Pts',(-8.79274596856292,1.00855506527731,16.4043814034892));
#30575=CARTESIAN_POINT('Ctrl Pts',(-8.95572220361263,0.961249135131234,
16.4120993771056));
#30576=CARTESIAN_POINT('Ctrl Pts',(-9.106998106675,0.873633747141485,16.419817350722));
#30577=CARTESIAN_POINT('Ctrl Pts',(-9.22913238736914,0.755810480769922,
16.4275353243383));
#30578=CARTESIAN_POINT('Ctrl Pts',(-9.35126666806328,0.637987214398357,
16.4352532979547));
#30579=CARTESIAN_POINT('Ctrl Pts',(-9.44425932638919,0.489956069644978,
16.4429712715711));
#30580=CARTESIAN_POINT('Ctrl Pts',(-9.49738881624737,0.328784230496411,
16.4506892451874));
#30581=CARTESIAN_POINT('Ctrl Pts',(-9.53227575775345,0.222952374406485,
16.4557571744075));
#30582=CARTESIAN_POINT('Ctrl Pts',(-9.54997466077663,0.111454567273571,
16.4608251036276));
#30583=CARTESIAN_POINT('Ctrl Pts',(-9.55005247215833,-1.9100347204657E-5,
16.4658930328476));
#30584=CARTESIAN_POINT('Origin',(-8.5,0.,15.5374873996035));
#30585=CARTESIAN_POINT('',(-9.71736724280504,-1.11660654972812E-5,17.1625126003965));
#30586=CARTESIAN_POINT('',(-9.71748246977037,-2.53252437245375E-5,17.1874873996035));
#30587=CARTESIAN_POINT('',(-9.71745,1.66304456946628E-15,15.5374873996035));
#30588=CARTESIAN_POINT('',(-8.18521110449555,1.17604951161381,17.4));
#30589=CARTESIAN_POINT('Ctrl Pts',(-9.71748246977038,-2.53252437245645E-5,
17.1874873996035));
#30590=CARTESIAN_POINT('Ctrl Pts',(-9.71751497142563,-0.0351019928070867,
17.1888631705217));
#30591=CARTESIAN_POINT('Ctrl Pts',(-9.70768334098354,-0.266938032321857,
17.1979569150563));
#30592=CARTESIAN_POINT('Ctrl Pts',(-9.56507989669121,-0.68475363956845,
17.2147686332073));
#30593=CARTESIAN_POINT('Ctrl Pts',(-9.12308418289996,-1.1022924873685,17.2379225540564));
#30594=CARTESIAN_POINT('Ctrl Pts',(-8.53741084518169,-1.26565584737736,
17.2610764749055));
#30595=CARTESIAN_POINT('Ctrl Pts',(-7.94311359864215,-1.13717035634921,
17.2842303957546));
#30596=CARTESIAN_POINT('Ctrl Pts',(-7.47722268493459,-0.746471406749234,
17.3073843166036));
#30597=CARTESIAN_POINT('Ctrl Pts',(-7.24718561960605,-0.183633649692887,
17.3305382374527));
#30598=CARTESIAN_POINT('Ctrl Pts',(-7.3060079723258,0.421518864292242,17.3536921583018));
#30599=CARTESIAN_POINT('Ctrl Pts',(-7.64021327215519,0.929515170005604,
17.3768460791509));
#30600=CARTESIAN_POINT('Ctrl Pts',(-7.99510874416169,1.12516550422184,17.3922820263836));
#30601=CARTESIAN_POINT('Ctrl Pts',(-8.18521110449555,1.17604951161381,17.4));
#30602=CARTESIAN_POINT('',(-8.81478889550434,1.17604951161384,17.4));
#30603=CARTESIAN_POINT('Origin',(-8.5,0.,17.4));
#30604=CARTESIAN_POINT('Ctrl Pts',(-9.71736724280504,-1.11660654973089E-5,
17.1625126003965));
#30605=CARTESIAN_POINT('Ctrl Pts',(-9.71739603884099,-0.0846136171028923,
17.1658299588182));
#30606=CARTESIAN_POINT('Ctrl Pts',(-9.68844277423369,-0.366027787036859,
17.1768652908563));
#30607=CARTESIAN_POINT('Ctrl Pts',(-9.47383591978867,-0.809275294625564,
17.1956185965107));
#30608=CARTESIAN_POINT('Ctrl Pts',(-8.98431387179416,-1.16992433712962,
17.2187725173598));
#30609=CARTESIAN_POINT('Ctrl Pts',(-8.38311431128619,-1.26080160014802,
17.2419264382089));
#30610=CARTESIAN_POINT('Ctrl Pts',(-7.80886733385048,-1.06095167099359,
17.265080359058));
#30611=CARTESIAN_POINT('Ctrl Pts',(-7.39398798803169,-0.616457995871644,
17.2882342799071));
#30612=CARTESIAN_POINT('Ctrl Pts',(-7.23414304365684,-0.0298154777491022,
17.3113882007562));
#30613=CARTESIAN_POINT('Ctrl Pts',(-7.36619075960647,0.563701428344329,
17.3345421216053));
#30614=CARTESIAN_POINT('Ctrl Pts',(-7.75968288434054,1.02723654746506,17.3576960424544));
#30615=CARTESIAN_POINT('Ctrl Pts',(-8.29136184904107,1.24083350426797,17.3795153352526));
#30616=CARTESIAN_POINT('Ctrl Pts',(-8.65756927545989,1.21801527236963,17.3936166544345));
#30617=CARTESIAN_POINT('Ctrl Pts',(-8.81482206889626,1.17607882593354,17.4));
#30618=CARTESIAN_POINT('Origin',(-8.5,0.,15.5374873996035));
#30619=CARTESIAN_POINT('',(-9.71737871990645,-1.72188190057376E-5,16.8625126003965));
#30620=CARTESIAN_POINT('',(-9.71750560220144,-2.14937386861674E-5,16.8874873996035));
#30621=CARTESIAN_POINT('',(-9.71745,1.66304456946628E-15,15.5374873996035));
#30622=CARTESIAN_POINT('Ctrl Pts',(-9.71750560220144,-2.1493738686134E-5,
16.8874873996035));
#30623=CARTESIAN_POINT('Ctrl Pts',(-9.71752782371263,-0.0265897765865916,
16.888529513509));
#30624=CARTESIAN_POINT('Ctrl Pts',(-9.71035795599032,-0.249912775849858,
16.8972896010309));
#30625=CARTESIAN_POINT('Ctrl Pts',(-9.57920029690692,-0.66227603951712,
16.9137676621692));
#30626=CARTESIAN_POINT('Ctrl Pts',(-9.14605408022473,-1.08898896173995,
16.9369215830183));
#30627=CARTESIAN_POINT('Ctrl Pts',(-8.56393482767032,-1.26459288749884,
16.9600755038673));
#30628=CARTESIAN_POINT('Ctrl Pts',(-7.96707289994234,-1.1485954638407,16.9832294247164));
#30629=CARTESIAN_POINT('Ctrl Pts',(-7.49309815860203,-0.767744433222239,
17.0063833455655));
#30630=CARTESIAN_POINT('Ctrl Pts',(-7.25130401707404,-0.209859896869422,
17.0295372664146));
#30631=CARTESIAN_POINT('Ctrl Pts',(-7.29744557308788,0.396416047559612,
17.0526911872637));
#30632=CARTESIAN_POINT('Ctrl Pts',(-7.62088308273839,0.911282765764439,
17.0758451081128));
#30633=CARTESIAN_POINT('Ctrl Pts',(-8.14703538592992,1.21601760624665,17.0989990289619));
#30634=CARTESIAN_POINT('Ctrl Pts',(-8.75457747423087,1.24035201730987,17.122152949811));
#30635=CARTESIAN_POINT('Ctrl Pts',(-9.30341679390951,0.978674783003138,
17.14530687066));
#30636=CARTESIAN_POINT('Ctrl Pts',(-9.64539351645688,0.520283291202953,
17.1670850205909));
#30637=CARTESIAN_POINT('Ctrl Pts',(-9.71733263953124,0.161675531135822,
17.1811451969054));
#30638=CARTESIAN_POINT('Ctrl Pts',(-9.71748246977038,-2.53252437245645E-5,
17.1874873996035));
#30639=CARTESIAN_POINT('Ctrl Pts',(-9.71737871990645,-1.72188190057931E-5,
16.8625126003965));
#30640=CARTESIAN_POINT('Ctrl Pts',(-9.71741919686537,-0.0761083706980662,
16.8654963018055));
#30641=CARTESIAN_POINT('Ctrl Pts',(-9.69220246389315,-0.348998849073912,
16.8761979768309));
#30642=CARTESIAN_POINT('Ctrl Pts',(-9.49058656515595,-0.788683177200059,
16.8946176254726));
#30643=CARTESIAN_POINT('Ctrl Pts',(-9.0087322805331,-1.15951471047599,16.9177715463217));
#30644=CARTESIAN_POINT('Ctrl Pts',(-8.40956987168007,-1.26297477764059,
16.9409254671708));
#30645=CARTESIAN_POINT('Ctrl Pts',(-7.83125966571002,-1.07520661380189,
16.9640793880199));
#30646=CARTESIAN_POINT('Ctrl Pts',(-7.40715369881707,-0.639507512896534,
16.987233308869));
#30647=CARTESIAN_POINT('Ctrl Pts',(-7.23504618881006,-0.0563449432224961,
17.010387229718));
#30648=CARTESIAN_POINT('Ctrl Pts',(-7.35462325340267,0.539810156841002,
17.0335411505671));
#30649=CARTESIAN_POINT('Ctrl Pts',(-7.73831172357029,1.01149091274223,17.0566950714162));
#30650=CARTESIAN_POINT('Ctrl Pts',(-8.29763721617962,1.24993287858306,17.0798489922653));
#30651=CARTESIAN_POINT('Ctrl Pts',(-8.90362536310944,1.20015393300998,17.1030029131144));
#30652=CARTESIAN_POINT('Ctrl Pts',(-9.41654189659505,0.873632559821981,
17.1261568339635));
#30653=CARTESIAN_POINT('Ctrl Pts',(-9.67490638243313,0.421305704246767,
17.1459933963908));
#30654=CARTESIAN_POINT('Ctrl Pts',(-9.71732904365461,0.112217536477445,
17.1581119852019));
#30655=CARTESIAN_POINT('Ctrl Pts',(-9.71736724280504,-1.11660654973089E-5,
17.1625126003965));
#30656=CARTESIAN_POINT('Origin',(-8.5,0.,15.5374873996035));
#30657=CARTESIAN_POINT('',(-9.71739489784702,-2.21442888292955E-5,16.5625126003965));
#30658=CARTESIAN_POINT('',(-9.71752534862784,-1.58793637348338E-5,16.5874873996035));
#30659=CARTESIAN_POINT('',(-9.71745,1.66304456946628E-15,15.5374873996035));
#30660=CARTESIAN_POINT('Ctrl Pts',(-9.71752534862784,-1.5879363734872E-5,
16.5874873996035));
#30661=CARTESIAN_POINT('Ctrl Pts',(-9.71753738116228,-0.0180768584738382,
16.5881958564963));
#30662=CARTESIAN_POINT('Ctrl Pts',(-9.71285071230468,-0.232889024209207,
16.5966222870055));
#30663=CARTESIAN_POINT('Ctrl Pts',(-9.59284627947019,-0.639507500190754,
16.612766691131));
#30664=CARTESIAN_POINT('Ctrl Pts',(-9.1687403210034,-1.07520659243964,16.6359206119801));
#30665=CARTESIAN_POINT('Ctrl Pts',(-8.59043012652324,-1.26297475254772,
16.6590745328292));
#30666=CARTESIAN_POINT('Ctrl Pts',(-7.99126772957441,-1.15951468743868,
16.6822284536783));
#30667=CARTESIAN_POINT('Ctrl Pts',(-7.50941345452508,-0.788683161530444,
16.7053823745274));
#30668=CARTESIAN_POINT('Ctrl Pts',(-7.2559776502202,-0.235989886660555,
16.7285362953765));
#30669=CARTESIAN_POINT('Ctrl Pts',(-7.28939985343257,0.371120086345011,
16.7516902162256));
#30670=CARTESIAN_POINT('Ctrl Pts',(-7.60197326804091,0.892653808620445,
16.7748441370746));
#30671=CARTESIAN_POINT('Ctrl Pts',(-8.12162186829395,1.20835128286614,16.7979980579237));
#30672=CARTESIAN_POINT('Ctrl Pts',(-8.72852034550391,1.24541610919772,16.8211519787728));
#30673=CARTESIAN_POINT('Ctrl Pts',(-9.28272451943119,0.995301542266061,
16.8443058996219));
#30674=CARTESIAN_POINT('Ctrl Pts',(-9.63962067752837,0.537268072859732,
16.8664177065655));
#30675=CARTESIAN_POINT('Ctrl Pts',(-9.71736324953685,0.170176915580277,
16.8808115398927));
#30676=CARTESIAN_POINT('Ctrl Pts',(-9.71750560220144,-2.1493738686134E-5,
16.8874873996035));
#30677=CARTESIAN_POINT('Ctrl Pts',(-9.71739489784702,-2.2144288829358E-5,
16.5625126003965));
#30678=CARTESIAN_POINT('Ctrl Pts',(-9.71744207005576,-0.0676017066010113,
16.5651626447928));
#30679=CARTESIAN_POINT('Ctrl Pts',(-9.69577211517131,-0.331969647279349,
16.5755306628055));
#30680=CARTESIAN_POINT('Ctrl Pts',(-9.50690186140351,-0.767744448476627,
16.5936166544345));
#30681=CARTESIAN_POINT('Ctrl Pts',(-9.0329271106457,-1.14859548666069,16.6167705752836));
#30682=CARTESIAN_POINT('Ctrl Pts',(-8.4360651710595,-1.26459291262403,16.6399244961327));
#30683=CARTESIAN_POINT('Ctrl Pts',(-7.85394590693938,-1.08898898337596,
16.6630784169817));
#30684=CARTESIAN_POINT('Ctrl Pts',(-7.42079968165148,-0.662276052675294,
16.6862323378308));
#30685=CARTESIAN_POINT('Ctrl Pts',(-7.23650529822705,-0.0828494758703863,
16.7093862586799));
#30686=CARTESIAN_POINT('Ctrl Pts',(-7.34355903464176,0.515681287920065,
16.732540179529));
#30687=CARTESIAN_POINT('Ctrl Pts',(-7.71727546501759,0.995301562040781,
16.7556941003781));
#30688=CARTESIAN_POINT('Ctrl Pts',(-8.27147964995585,1.24541613394172,16.7788480212272));
#30689=CARTESIAN_POINT('Ctrl Pts',(-8.8783781392237,1.20835130687373,16.8020019420763));
#30690=CARTESIAN_POINT('Ctrl Pts',(-9.39802674980115,0.892653826355733,
16.8251558629254));
#30691=CARTESIAN_POINT('Ctrl Pts',(-9.67032078285669,0.438326893942781,
16.8453260823654));
#30692=CARTESIAN_POINT('Ctrl Pts',(-9.7173144946656,0.120717458075642,16.8577783281891));
#30693=CARTESIAN_POINT('Ctrl Pts',(-9.71737871990645,-1.72188190057931E-5,
16.8625126003965));
#30694=CARTESIAN_POINT('Origin',(-8.5,0.,15.5374873996035));
#30695=CARTESIAN_POINT('',(-9.71741527458843,-3.00182063334153E-5,16.2625126003965));
#30696=CARTESIAN_POINT('',(-9.71753950048363,-8.82892751896623E-6,16.2874873996035));
#30697=CARTESIAN_POINT('',(-9.71745,1.66304456946628E-15,15.5374873996035));
#30698=CARTESIAN_POINT('',(-8.81478889550445,1.17604951161381,16.2));
#30699=CARTESIAN_POINT('Ctrl Pts',(-8.81478889550445,1.17604951161381,16.2));
#30700=CARTESIAN_POINT('Ctrl Pts',(-9.00489125583831,1.12516550422184,16.2077179736164));
#30701=CARTESIAN_POINT('Ctrl Pts',(-9.35978667802179,0.929514905730451,
16.2231539208491));
#30702=CARTESIAN_POINT('Ctrl Pts',(-9.66055713486829,0.472340269425348,
16.2439914543146));
#30703=CARTESIAN_POINT('Ctrl Pts',(-9.7173031168173,0.137707734298517,16.2571110141637));
#30704=CARTESIAN_POINT('Ctrl Pts',(-9.71741527458843,-3.00182063335264E-5,
16.2625126003965));
#30705=CARTESIAN_POINT('',(-8.18517792975417,1.1760787964605,16.2));
#30706=CARTESIAN_POINT('Origin',(-8.5,0.,16.2));
#30707=CARTESIAN_POINT('Ctrl Pts',(-8.18517792975417,1.1760787964605,16.2));
#30708=CARTESIAN_POINT('Ctrl Pts',(-8.34243072315718,1.21801524478933,16.2063833455655));
#30709=CARTESIAN_POINT('Ctrl Pts',(-8.70863814132373,1.24083347266754,16.2204846647474));
#30710=CARTESIAN_POINT('Ctrl Pts',(-9.24031710111236,1.02723652833138,16.2423039575456));
#30711=CARTESIAN_POINT('Ctrl Pts',(-9.62743963500528,0.571204805999074,
16.2650830785146));
#30712=CARTESIAN_POINT('Ctrl Pts',(-9.71746327074259,0.187187292270235,
16.2801442258672));
#30713=CARTESIAN_POINT('Ctrl Pts',(-9.71753950048363,-8.82892751894945E-6,
16.2874873996035));
#30714=CARTESIAN_POINT('Origin',(-8.5,0.,15.5374873996035));
#30715=CARTESIAN_POINT('Ctrl Pts',(-9.71753950048363,-8.82892751894945E-6,
16.2874873996035));
#30716=CARTESIAN_POINT('Ctrl Pts',(-9.71754339129418,-0.00956342838294255,
16.2878621994836));
#30717=CARTESIAN_POINT('Ctrl Pts',(-9.71516274507233,-0.215866810278111,
16.2959549729801));
#30718=CARTESIAN_POINT('Ctrl Pts',(-9.60601198986148,-0.616457983927628,
16.3117657200929));
#30719=CARTESIAN_POINT('Ctrl Pts',(-9.19113265245436,-1.06095164978761,
16.334919640942));
#30720=CARTESIAN_POINT('Ctrl Pts',(-8.61688568636888,-1.26080157516723,
16.3580735617911));
#30721=CARTESIAN_POINT('Ctrl Pts',(-8.01568613783619,-1.16992431385386,
16.3812274826402));
#30722=CARTESIAN_POINT('Ctrl Pts',(-7.52616409955547,-0.809275278562791,
16.4043814034892));
#30723=CARTESIAN_POINT('Ctrl Pts',(-7.26119801228416,-0.26201616100183,
16.4275353243383));
#30724=CARTESIAN_POINT('Ctrl Pts',(-7.28188617544855,0.345661023092506,
16.4506892451874));
#30725=CARTESIAN_POINT('Ctrl Pts',(-7.58345812161518,0.873632542466389,
16.4738431660365));
#30726=CARTESIAN_POINT('Ctrl Pts',(-8.09637464490968,1.20015390916439,16.4969970868856));
#30727=CARTESIAN_POINT('Ctrl Pts',(-8.7023627797999,1.24993285374973,16.5201510077347));
#30728=CARTESIAN_POINT('Ctrl Pts',(-9.26168826129643,1.01149089264566,16.5433049285838));
#30729=CARTESIAN_POINT('Ctrl Pts',(-9.63363673657241,0.554242495534025,
16.56575039254));
#30730=CARTESIAN_POINT('Ctrl Pts',(-9.71740629798092,0.178680575422754,
16.5804778828799));
#30731=CARTESIAN_POINT('Ctrl Pts',(-9.71752534862784,-1.5879363734872E-5,
16.5874873996035));
#30732=CARTESIAN_POINT('Ctrl Pts',(-9.71741527458843,-3.00182063335264E-5,
16.2625126003965));
#30733=CARTESIAN_POINT('Ctrl Pts',(-9.71746337172782,-0.059096740164705,
16.2648289877801));
#30734=CARTESIAN_POINT('Ctrl Pts',(-9.69914896928468,-0.314938316431683,
16.27486334878));
#30735=CARTESIAN_POINT('Ctrl Pts',(-9.52277733259636,-0.746471423726082,
16.2926156833963));
#30736=CARTESIAN_POINT('Ctrl Pts',(-9.05688641176464,-1.13717038838356,
16.3157696042454));
#30737=CARTESIAN_POINT('Ctrl Pts',(-8.46258915349396,-1.26565587137657,
16.3389235250945));
#30738=CARTESIAN_POINT('Ctrl Pts',(-7.87691580481983,-1.10229251092252,
16.3620774459436));
#30739=CARTESIAN_POINT('Ctrl Pts',(-7.43492008199845,-0.684753652714294,
16.3852313667927));
#30740=CARTESIAN_POINT('Ctrl Pts',(-7.23851963711968,-0.109317543695422,
16.4083852876418));
#30741=CARTESIAN_POINT('Ctrl Pts',(-7.33300308119116,0.491325759444495,
16.4315392084909));
#30742=CARTESIAN_POINT('Ctrl Pts',(-7.69658319014803,0.978674802377791,
16.45469312934));
#30743=CARTESIAN_POINT('Ctrl Pts',(-8.24542252070005,1.24035204198393,16.477847050189));
#30744=CARTESIAN_POINT('Ctrl Pts',(-8.85296462108838,1.21601763039105,16.5010009710381));
#30745=CARTESIAN_POINT('Ctrl Pts',(-9.37911693472505,0.911282783877038,
16.5241548918872));
#30746=CARTESIAN_POINT('Ctrl Pts',(-9.66553593534035,0.455344290414368,
16.54465876834));
#30747=CARTESIAN_POINT('Ctrl Pts',(-9.7173046859942,0.129216610729656,16.5574446711764));
#30748=CARTESIAN_POINT('Ctrl Pts',(-9.71739489784702,-2.2144288829358E-5,
16.5625126003965));
#30749=CARTESIAN_POINT('Ctrl Pts',(-7.70661869325987,-0.687936125025659,
16.2));
#30750=CARTESIAN_POINT('Ctrl Pts',(-7.59541735366078,-0.559690113640392,
16.2077179736164));
#30751=CARTESIAN_POINT('Ctrl Pts',(-7.43647780937234,-0.248368218683425,
16.2231539208491));
#30752=CARTESIAN_POINT('Ctrl Pts',(-7.44330902884952,0.276075381285195,
16.2463078416982));
#30753=CARTESIAN_POINT('Ctrl Pts',(-7.69382549331944,0.73679971847695,16.2694617625473));
#30754=CARTESIAN_POINT('Ctrl Pts',(-8.1302325908592,1.02765943396112,16.2926156833963));
#30755=CARTESIAN_POINT('Ctrl Pts',(-8.65190784365933,1.0815384208056,16.3157696042454));
#30756=CARTESIAN_POINT('Ctrl Pts',(-9.13855352406923,0.886033166372978,
16.3389235250945));
#30757=CARTESIAN_POINT('Ctrl Pts',(-9.47795643253951,0.486215332577987,
16.3620774459436));
#30758=CARTESIAN_POINT('Ctrl Pts',(-9.59185294146457,-0.0257170578466189,
16.3852313667927));
#30759=CARTESIAN_POINT('Ctrl Pts',(-9.45398019676664,-0.531720012257096,
16.4083852876418));
#30760=CARTESIAN_POINT('Ctrl Pts',(-9.09612994237326,-0.915113825982153,
16.4315392084909));
#30761=CARTESIAN_POINT('Ctrl Pts',(-8.60081864491845,-1.0874924917517,16.4546931293399));
#30762=CARTESIAN_POINT('Ctrl Pts',(-8.08225965201181,-1.0091071682434,16.4778470501891));
#30763=CARTESIAN_POINT('Ctrl Pts',(-7.66002704089959,-0.698032748793615,
16.5010009710381));
#30764=CARTESIAN_POINT('Ctrl Pts',(-7.43148304464216,-0.225999565212552,
16.5241548918872));
#30765=CARTESIAN_POINT('Ctrl Pts',(-7.44932742440225,0.298146651073506,
16.5473088127363));
#30766=CARTESIAN_POINT('Ctrl Pts',(-7.70944545854705,0.753543498988833,
16.5704627335854));
#30767=CARTESIAN_POINT('Ctrl Pts',(-8.15185676177228,1.03518142019264,16.5936166544345));
#30768=CARTESIAN_POINT('Ctrl Pts',(-8.67454610461857,1.07811777873637,16.6167705752836));
#30769=CARTESIAN_POINT('Ctrl Pts',(-9.15698701645849,0.872451917012778,
16.6399244961327));
#30770=CARTESIAN_POINT('Ctrl Pts',(-9.48793387630323,0.465608143608788,
16.6630784169817));
#30771=CARTESIAN_POINT('Ctrl Pts',(-9.59107394204218,-0.0485997976939159,
16.6862323378308));
#30772=CARTESIAN_POINT('Ctrl Pts',(-9.44262423760454,-0.551601154832076,
16.7093862586799));
#30773=CARTESIAN_POINT('Ctrl Pts',(-9.07681564835161,-0.927409292144124,
16.732540179529));
#30774=CARTESIAN_POINT('Ctrl Pts',(-8.57799965161777,-1.08936694537793,
16.7556941003781));
#30775=CARTESIAN_POINT('Ctrl Pts',(-8.0611977845711,-1.00012844328667,16.7788480212272));
#30776=CARTESIAN_POINT('Ctrl Pts',(-7.64557893022037,-0.680271212717664,
16.8020019420763));
#30777=CARTESIAN_POINT('Ctrl Pts',(-7.42698027064457,-0.203550848069529,
16.8251558629253));
#30778=CARTESIAN_POINT('Ctrl Pts',(-7.45580827638879,0.320106125648607,
16.8483097837744));
#30779=CARTESIAN_POINT('Ctrl Pts',(-7.725415523241,0.769950112474704,16.8714637046235));
#30780=CARTESIAN_POINT('Ctrl Pts',(-8.17363351586963,1.04225198746374,16.8946176254726));
#30781=CARTESIAN_POINT('Ctrl Pts',(-8.69710806588661,1.0742219033788,16.9177715463217));
#30782=CARTESIAN_POINT('Ctrl Pts',(-9.17513164224789,0.85848794573378,16.9409254671708));
#30783=CARTESIAN_POINT('Ctrl Pts',(-9.49747721351624,0.444796016005563,
16.9640793880199));
#30784=CARTESIAN_POINT('Ctrl Pts',(-9.58981540101927,-0.0714610315684377,
16.987233308869));
#30785=CARTESIAN_POINT('Ctrl Pts',(-9.43085402421615,-0.571239943403776,
17.0103872297181));
#30786=CARTESIAN_POINT('Ctrl Pts',(-9.05724784561501,-0.939297144624521,
17.0335411505671));
#30787=CARTESIAN_POINT('Ctrl Pts',(-8.55514638181166,-1.09076265239848,
17.0566950714162));
#30788=CARTESIAN_POINT('Ctrl Pts',(-8.04032876276599,-0.990710170092501,
17.0798489922653));
#30789=CARTESIAN_POINT('Ctrl Pts',(-7.63150632580228,-0.662210710359089,
17.1030029131144));
#30790=CARTESIAN_POINT('Ctrl Pts',(-7.42294907251177,-0.181012672144712,
17.1261568339635));
#30791=CARTESIAN_POINT('Ctrl Pts',(-7.46274803589435,0.341924918101235,
17.1493107548126));
#30792=CARTESIAN_POINT('Ctrl Pts',(-7.74172600532555,0.786018343528881,
17.1724646756617));
#30793=CARTESIAN_POINT('Ctrl Pts',(-8.19555370550331,1.04886450229546,17.1956185965107));
#30794=CARTESIAN_POINT('Ctrl Pts',(-8.71958339618863,1.06985391874582,17.2187725173598));
#30795=CARTESIAN_POINT('Ctrl Pts',(-9.19297956818299,0.844146691553324,
17.2419264382089));
#30796=CARTESIAN_POINT('Ctrl Pts',(-9.50658215125916,0.423788385239755,
17.265080359058));
#30797=CARTESIAN_POINT('Ctrl Pts',(-9.58807795211741,-0.0942908127739469,
17.2882342799071));
#30798=CARTESIAN_POINT('Ctrl Pts',(-9.41867460636201,-0.590627785051402,
17.3113882007562));
#30799=CARTESIAN_POINT('Ctrl Pts',(-9.03743537760339,-0.950771975017998,
17.3345421216053));
#30800=CARTESIAN_POINT('Ctrl Pts',(-8.53226837120644,-1.09167949840319,
17.3576960424544));
#30801=CARTESIAN_POINT('Ctrl Pts',(-8.01966289369923,-0.980855551523517,
17.3808499633034));
#30802=CARTESIAN_POINT('Ctrl Pts',(-7.61781308591713,-0.643861862275552,
17.4040038841525));
#30803=CARTESIAN_POINT('Ctrl Pts',(-7.41939678766957,-0.158391470321163,
17.4271578050016));
#30804=CARTESIAN_POINT('Ctrl Pts',(-7.47013345249442,0.36357711560498,17.4503117258507));
#30805=CARTESIAN_POINT('Ctrl Pts',(-7.75839907765424,0.801744531621737,
17.4734656466998));
#30806=CARTESIAN_POINT('Ctrl Pts',(-8.06451081542912,0.970500879693911,
17.4889015939325));
#30807=CARTESIAN_POINT('Ctrl Pts',(-8.22848181102368,1.01439039972538,17.4966195675489));
#30808=CARTESIAN_POINT('Ctrl Pts',(-7.66447275106929,-0.724480616192546,
16.1677934774837));
#30809=CARTESIAN_POINT('Ctrl Pts',(-7.54736418225968,-0.589421929822254,
16.1755114511001));
#30810=CARTESIAN_POINT('Ctrl Pts',(-7.37998146343654,-0.261562016542889,
16.1909473983328));
#30811=CARTESIAN_POINT('Ctrl Pts',(-7.38717557044174,0.290741036955474,
16.2141013191819));
#30812=CARTESIAN_POINT('Ctrl Pts',(-7.65099995172245,0.775939937785307,
16.237255240031));
#30813=CARTESIAN_POINT('Ctrl Pts',(-8.11058983432182,1.08225068123072,16.26040916088));
#30814=CARTESIAN_POINT('Ctrl Pts',(-8.65997748072132,1.13899182356782,16.2835630817291));
#30815=CARTESIAN_POINT('Ctrl Pts',(-9.17247471641694,0.933100953692445,
16.3067170025782));
#30816=CARTESIAN_POINT('Ctrl Pts',(-9.52990736070048,0.512044026958499,
16.3298709234273));
#30817=CARTESIAN_POINT('Ctrl Pts',(-9.64985427141858,-0.0270831974620941,
16.3530248442764));
#30818=CARTESIAN_POINT('Ctrl Pts',(-9.50465746113159,-0.55996600281394,
16.3761787651255));
#30819=CARTESIAN_POINT('Ctrl Pts',(-9.12779751240029,-0.963726433917306,
16.3993326859746));
#30820=CARTESIAN_POINT('Ctrl Pts',(-8.60617432540192,-1.14526218622354,
16.4224866068237));
#30821=CARTESIAN_POINT('Ctrl Pts',(-8.06006848061994,-1.06271288344689,
16.4456405276728));
#30822=CARTESIAN_POINT('Ctrl Pts',(-7.61540606045155,-0.735113592050007,
16.4687944485218));
#30823=CARTESIAN_POINT('Ctrl Pts',(-7.3747213671895,-0.238005097142311,
16.4919483693709));
#30824=CARTESIAN_POINT('Ctrl Pts',(-7.39351367475101,0.31398477507984,16.51510229022));
#30825=CARTESIAN_POINT('Ctrl Pts',(-7.66744967956976,0.793573180148018,
16.5382562110691));
#30826=CARTESIAN_POINT('Ctrl Pts',(-8.13336272281808,1.09017224984989,16.5614101319182));
#30827=CARTESIAN_POINT('Ctrl Pts',(-8.68381832967901,1.13538947040749,16.5845640527673));
#30828=CARTESIAN_POINT('Ctrl Pts',(-9.19188743140447,0.918798242223738,
16.6077179736164));
#30829=CARTESIAN_POINT('Ctrl Pts',(-9.54041482548246,0.490342144444559,
16.6308718944655));
#30830=CARTESIAN_POINT('Ctrl Pts',(-9.64903389004738,-0.0511815124969747,
16.6540258153145));
#30831=CARTESIAN_POINT('Ctrl Pts',(-9.49269825155976,-0.580903269951635,
16.6771797361636));
#30832=CARTESIAN_POINT('Ctrl Pts',(-9.1074572059022,-0.976675058909296,
16.7003336570127));
#30833=CARTESIAN_POINT('Ctrl Pts',(-8.58214314325293,-1.14723621443453,
16.7234875778618));
#30834=CARTESIAN_POINT('Ctrl Pts',(-8.03788776623887,-1.05325719133734,
16.7466414987109));
#30835=CARTESIAN_POINT('Ctrl Pts',(-7.60019043832194,-0.71640852898859,
16.76979541956));
#30836=CARTESIAN_POINT('Ctrl Pts',(-7.36997939716978,-0.214363860933204,
16.7929493404091));
#30837=CARTESIAN_POINT('Ctrl Pts',(-7.40033880207005,0.337110779214075,
16.8161032612581));
#30838=CARTESIAN_POINT('Ctrl Pts',(-7.68426810484097,0.810851344523284,
16.8392571821072));
#30839=CARTESIAN_POINT('Ctrl Pts',(-8.15629630001107,1.09761841926454,16.8624111029563));
#30840=CARTESIAN_POINT('Ctrl Pts',(-8.70757882575904,1.13128663865177,16.8855650238054));
#30841=CARTESIAN_POINT('Ctrl Pts',(-9.21099593464233,0.904092477911206,
16.9087189446545));
#30842=CARTESIAN_POINT('Ctrl Pts',(-9.55046512313816,0.468424436561869,
16.9318728655036));
#30843=CARTESIAN_POINT('Ctrl Pts',(-9.64770849290277,-0.0752571791204098,
16.9550267863527));
#30844=CARTESIAN_POINT('Ctrl Pts',(-9.48030278177974,-0.601585308774891,
16.9781807072017));
#30845=CARTESIAN_POINT('Ctrl Pts',(-9.08684992381825,-0.989194416996331,
17.0013346280508));
#30846=CARTESIAN_POINT('Ctrl Pts',(-8.55807586376454,-1.1487060640986,17.0244885488999));
#30847=CARTESIAN_POINT('Ctrl Pts',(-8.01591014182478,-1.0433386013419,17.047642469749));
#30848=CARTESIAN_POINT('Ctrl Pts',(-7.58537027006887,-0.697388617980139,
17.0707963905981));
#30849=CARTESIAN_POINT('Ctrl Pts',(-7.36573405403253,-0.190628413719615,
17.0939503114472));
#30850=CARTESIAN_POINT('Ctrl Pts',(-7.40764721495886,0.360088627920694,
17.1171042322963));
#30851=CARTESIAN_POINT('Ctrl Pts',(-7.70144503112983,0.827773150940734,
17.1402581531454));
#30852=CARTESIAN_POINT('Ctrl Pts',(-8.17938093231218,1.10458220361253,17.1634120739944));
#30853=CARTESIAN_POINT('Ctrl Pts',(-8.73124808886938,1.12668661826717,17.1865659948435));
#30854=CARTESIAN_POINT('Ctrl Pts',(-9.22979197675849,0.888989388703262,
17.2097199156926));
#30855=CARTESIAN_POINT('Ctrl Pts',(-9.56005373270004,0.446300840012277,
17.2328738365417));
#30856=CARTESIAN_POINT('Ctrl Pts',(-9.64587874737083,-0.0992997222485111,
17.2560277573908));
#30857=CARTESIAN_POINT('Ctrl Pts',(-9.46747636980508,-0.622003069890418,
17.2791816782399));
#30858=CARTESIAN_POINT('Ctrl Pts',(-9.06598497936891,-1.00127881246817,
17.302335599089));
#30859=CARTESIAN_POINT('Ctrl Pts',(-8.53398252919819,-1.14967161472792,
17.3254895199381));
#30860=CARTESIAN_POINT('Ctrl Pts',(-7.99414646201354,-1.03296048646541,
17.3486434407871));
#30861=CARTESIAN_POINT('Ctrl Pts',(-7.57094961892295,-0.678065043766779,
17.3717973616362));
#30862=CARTESIAN_POINT('Ctrl Pts',(-7.36199306498173,-0.166805530111738,
17.3949512824853));
#30863=CARTESIAN_POINT('Ctrl Pts',(-7.41542495910488,0.382891031834067,
17.4181052033344));
#30864=CARTESIAN_POINT('Ctrl Pts',(-7.71900380915456,0.844334744416359,
17.4412591241835));
#30865=CARTESIAN_POINT('Ctrl Pts',(-8.04137679167331,1.02205575453655,17.4566950714162));
#30866=CARTESIAN_POINT('Ctrl Pts',(-8.21405824218097,1.06827677035486,17.4644130450326));
#30867=CARTESIAN_POINT('Ctrl Pts',(-7.62232680887872,-0.761025107359433,
16.1355869549674));
#30868=CARTESIAN_POINT('Ctrl Pts',(-7.49931101085859,-0.619153746004116,
16.1433049285838));
#30869=CARTESIAN_POINT('Ctrl Pts',(-7.32348511750074,-0.274755814402354,
16.1587408758165));
#30870=CARTESIAN_POINT('Ctrl Pts',(-7.33104211203396,0.305406692625752,
16.1818947966656));
#30871=CARTESIAN_POINT('Ctrl Pts',(-7.60817441012546,0.815080157093664,
16.2050487175147));
#30872=CARTESIAN_POINT('Ctrl Pts',(-8.09094707778444,1.13684192850031,16.2282026383638));
#30873=CARTESIAN_POINT('Ctrl Pts',(-8.66804711778331,1.19644522633004,16.2513565592128));
#30874=CARTESIAN_POINT('Ctrl Pts',(-9.20639590876465,0.980168741011912,
16.2745104800619));
#30875=CARTESIAN_POINT('Ctrl Pts',(-9.58185828886143,0.537872721339012,
16.297664400911));
#30876=CARTESIAN_POINT('Ctrl Pts',(-9.70785560137258,-0.0284493370775698,
16.3208183217601));
#30877=CARTESIAN_POINT('Ctrl Pts',(-9.55533472549653,-0.588211993370783,
16.3439722426092));
#30878=CARTESIAN_POINT('Ctrl Pts',(-9.15946508242732,-1.01233904185246,
16.3671261634583));
#30879=CARTESIAN_POINT('Ctrl Pts',(-8.6115300058854,-1.20303188069538,16.3902800843074));
#30880=CARTESIAN_POINT('Ctrl Pts',(-8.03787730922807,-1.11631859865037,
16.4134340051565));
#30881=CARTESIAN_POINT('Ctrl Pts',(-7.57078508000351,-0.772194435306399,
16.4365879260055));
#30882=CARTESIAN_POINT('Ctrl Pts',(-7.31795968973683,-0.25001062907207,
16.4597418468546));
#30883=CARTESIAN_POINT('Ctrl Pts',(-7.33769992509978,0.329822899086172,
16.4828957677037));
#30884=CARTESIAN_POINT('Ctrl Pts',(-7.62545390059247,0.833602861307204,
16.5060496885528));
#30885=CARTESIAN_POINT('Ctrl Pts',(-8.11486868386388,1.14516307950714,16.5292036094019));
#30886=CARTESIAN_POINT('Ctrl Pts',(-8.69309055473946,1.19266116207861,16.552357530251));
#30887=CARTESIAN_POINT('Ctrl Pts',(-9.22678784635045,0.965144567434699,
16.5755114511001));
#30888=CARTESIAN_POINT('Ctrl Pts',(-9.5928957746617,0.515076145280332,16.5986653719492));
#30889=CARTESIAN_POINT('Ctrl Pts',(-9.70699383805257,-0.0537632273000342,
16.6218192927982));
#30890=CARTESIAN_POINT('Ctrl Pts',(-9.54277226551496,-0.610205385071195,
16.6449732136473));
#30891=CARTESIAN_POINT('Ctrl Pts',(-9.1380987634528,-1.02594082567447,16.6681271344964));
#30892=CARTESIAN_POINT('Ctrl Pts',(-8.58628663488808,-1.20510548349113,
16.6912810553455));
#30893=CARTESIAN_POINT('Ctrl Pts',(-8.01457774790664,-1.10638593938801,
16.7144349761946));
#30894=CARTESIAN_POINT('Ctrl Pts',(-7.55480194642351,-0.752545845259518,
16.7375888970437));
#30895=CARTESIAN_POINT('Ctrl Pts',(-7.31297852369499,-0.22517687379688,
16.7607428178928));
#30896=CARTESIAN_POINT('Ctrl Pts',(-7.3448693277513,0.354115432779543,16.7838967387418));
#30897=CARTESIAN_POINT('Ctrl Pts',(-7.64312068644094,0.851752576571865,
16.8070506595909));
#30898=CARTESIAN_POINT('Ctrl Pts',(-8.13895908415251,1.15298485106534,16.83020458044));
#30899=CARTESIAN_POINT('Ctrl Pts',(-8.71804958563147,1.18835137392474,16.8533585012891));
#30900=CARTESIAN_POINT('Ctrl Pts',(-9.24686022703676,0.949697010088635,
16.8765124221382));
#30901=CARTESIAN_POINT('Ctrl Pts',(-9.60345303276009,0.492052857118175,
16.8996663429873));
#30902=CARTESIAN_POINT('Ctrl Pts',(-9.70560158478626,-0.0790533266723822,
16.9228202638364));
#30903=CARTESIAN_POINT('Ctrl Pts',(-9.52975153934333,-0.631930674146006,
16.9459741846855));
#30904=CARTESIAN_POINT('Ctrl Pts',(-9.11645200202149,-1.03909168936814,
16.9691281055346));
#30905=CARTESIAN_POINT('Ctrl Pts',(-8.56100534571743,-1.20664947579872,
16.9922820263836));
#30906=CARTESIAN_POINT('Ctrl Pts',(-7.99149152088356,-1.0959670325913,17.0154359472327));
#30907=CARTESIAN_POINT('Ctrl Pts',(-7.53923421433545,-0.732566525601189,
17.0385898680818));
#30908=CARTESIAN_POINT('Ctrl Pts',(-7.30851903555328,-0.200244155294519,
17.0617437889309));
#30909=CARTESIAN_POINT('Ctrl Pts',(-7.35254639402337,0.378252337740153,
17.08489770978));
#30910=CARTESIAN_POINT('Ctrl Pts',(-7.66116405693411,0.869527958352586,
17.1080516306291));
#30911=CARTESIAN_POINT('Ctrl Pts',(-8.16320815912104,1.16029990492959,17.1312055514782));
#30912=CARTESIAN_POINT('Ctrl Pts',(-8.74291278155013,1.18351931778852,17.1543594723273));
#30913=CARTESIAN_POINT('Ctrl Pts',(-9.26660438533401,0.9338320858532,17.1775133931763));
#30914=CARTESIAN_POINT('Ctrl Pts',(-9.61352531414093,0.468813294784797,
17.2006673140254));
#30915=CARTESIAN_POINT('Ctrl Pts',(-9.70367954262425,-0.104308631723075,
17.2238212348745));
#30916=CARTESIAN_POINT('Ctrl Pts',(-9.51627813324814,-0.653378354729435,
17.2469751557236));
#30917=CARTESIAN_POINT('Ctrl Pts',(-9.09453458113444,-1.05178564991833,
17.2701290765727));
#30918=CARTESIAN_POINT('Ctrl Pts',(-8.53569668718994,-1.20766373105264,
17.2932829974218));
#30919=CARTESIAN_POINT('Ctrl Pts',(-7.96863003032785,-1.08506542140731,
17.3164369182709));
#30920=CARTESIAN_POINT('Ctrl Pts',(-7.52408615192877,-0.712268225258007,
17.3395908391199));
#30921=CARTESIAN_POINT('Ctrl Pts',(-7.30458934229389,-0.175219589902312,
17.362744759969));
#30922=CARTESIAN_POINT('Ctrl Pts',(-7.36071646571534,0.402204948063154,
17.3858986808181));
#30923=CARTESIAN_POINT('Ctrl Pts',(-7.67960854065487,0.886924957210982,
17.4090526016672));
#30924=CARTESIAN_POINT('Ctrl Pts',(-8.0182427679175,1.0736106293792,17.4244885488999));
#30925=CARTESIAN_POINT('Ctrl Pts',(-8.19963467333826,1.12216314098434,17.4322065225163));
#30926=CARTESIAN_POINT('Ctrl Pts',(-7.58018086668815,-0.797569598526321,
16.1033804324511));
#30927=CARTESIAN_POINT('Ctrl Pts',(-7.45125783945749,-0.648885562185978,
16.1110984060675));
#30928=CARTESIAN_POINT('Ctrl Pts',(-7.26698877156495,-0.287949612261818,
16.1265343533002));
#30929=CARTESIAN_POINT('Ctrl Pts',(-7.27490865362618,0.32007234829603,16.1496882741493));
#30930=CARTESIAN_POINT('Ctrl Pts',(-7.56534886852848,0.854220376402022,
16.1728421949984));
#30931=CARTESIAN_POINT('Ctrl Pts',(-8.07130432124706,1.1914331757699,16.1959961158475));
#30932=CARTESIAN_POINT('Ctrl Pts',(-8.6761167548453,1.25389862909226,16.2191500366966));
#30933=CARTESIAN_POINT('Ctrl Pts',(-9.24031710111236,1.02723652833138,16.2423039575456));
#30934=CARTESIAN_POINT('Ctrl Pts',(-9.6338092170224,0.563701415719523,16.2654578783947));
#30935=CARTESIAN_POINT('Ctrl Pts',(-9.76585693132658,-0.0298154766930449,
16.2886117992438));
#30936=CARTESIAN_POINT('Ctrl Pts',(-9.60601198986148,-0.616457983927628,
16.3117657200929));
#30937=CARTESIAN_POINT('Ctrl Pts',(-9.19113265245436,-1.06095164978761,
16.334919640942));
#30938=CARTESIAN_POINT('Ctrl Pts',(-8.61688568636888,-1.26080157516723,
16.3580735617911));
#30939=CARTESIAN_POINT('Ctrl Pts',(-8.01568613783619,-1.16992431385386,
16.3812274826402));
#30940=CARTESIAN_POINT('Ctrl Pts',(-7.52616409955547,-0.809275278562791,
16.4043814034892));
#30941=CARTESIAN_POINT('Ctrl Pts',(-7.26119801228416,-0.26201616100183,
16.4275353243383));
#30942=CARTESIAN_POINT('Ctrl Pts',(-7.28188617544855,0.345661023092506,
16.4506892451874));
#30943=CARTESIAN_POINT('Ctrl Pts',(-7.58345812161518,0.873632542466389,
16.4738431660365));
#30944=CARTESIAN_POINT('Ctrl Pts',(-8.09637464490968,1.20015390916439,16.4969970868856));
#30945=CARTESIAN_POINT('Ctrl Pts',(-8.7023627797999,1.24993285374973,16.5201510077347));
#30946=CARTESIAN_POINT('Ctrl Pts',(-9.26168826129643,1.01149089264566,16.5433049285838));
#30947=CARTESIAN_POINT('Ctrl Pts',(-9.64537672384094,0.539810146116103,
16.5664588494329));
#30948=CARTESIAN_POINT('Ctrl Pts',(-9.76495378605776,-0.0563449421030929,
16.5896127702819));
#30949=CARTESIAN_POINT('Ctrl Pts',(-9.59284627947019,-0.639507500190754,
16.612766691131));
#30950=CARTESIAN_POINT('Ctrl Pts',(-9.1687403210034,-1.07520659243964,16.6359206119801));
#30951=CARTESIAN_POINT('Ctrl Pts',(-8.59043012652324,-1.26297475254772,
16.6590745328292));
#30952=CARTESIAN_POINT('Ctrl Pts',(-7.99126772957441,-1.15951468743868,
16.6822284536783));
#30953=CARTESIAN_POINT('Ctrl Pts',(-7.50941345452508,-0.788683161530444,
16.7053823745274));
#30954=CARTESIAN_POINT('Ctrl Pts',(-7.2559776502202,-0.235989886660555,
16.7285362953765));
#30955=CARTESIAN_POINT('Ctrl Pts',(-7.28939985343257,0.371120086345011,
16.7516902162256));
#30956=CARTESIAN_POINT('Ctrl Pts',(-7.60197326804091,0.892653808620445,
16.7748441370746));
#30957=CARTESIAN_POINT('Ctrl Pts',(-8.12162186829395,1.20835128286614,16.7979980579237));
#30958=CARTESIAN_POINT('Ctrl Pts',(-8.72852034550391,1.24541610919772,16.8211519787728));
#30959=CARTESIAN_POINT('Ctrl Pts',(-9.28272451943119,0.995301542266061,
16.8443058996219));
#30960=CARTESIAN_POINT('Ctrl Pts',(-9.65644094238201,0.515681277674482,
16.867459820471));
#30961=CARTESIAN_POINT('Ctrl Pts',(-9.76349467666975,-0.0828494742243546,
16.8906137413201));
#30962=CARTESIAN_POINT('Ctrl Pts',(-9.57920029690692,-0.66227603951712,
16.9137676621692));
#30963=CARTESIAN_POINT('Ctrl Pts',(-9.14605408022473,-1.08898896173995,
16.9369215830183));
#30964=CARTESIAN_POINT('Ctrl Pts',(-8.56393482767032,-1.26459288749884,
16.9600755038673));
#30965=CARTESIAN_POINT('Ctrl Pts',(-7.96707289994234,-1.1485954638407,16.9832294247164));
#30966=CARTESIAN_POINT('Ctrl Pts',(-7.49309815860203,-0.767744433222239,
17.0063833455655));
#30967=CARTESIAN_POINT('Ctrl Pts',(-7.25130401707404,-0.209859896869422,
17.0295372664146));
#30968=CARTESIAN_POINT('Ctrl Pts',(-7.29744557308788,0.396416047559612,
17.0526911872637));
#30969=CARTESIAN_POINT('Ctrl Pts',(-7.62088308273839,0.911282765764439,
17.0758451081128));
#30970=CARTESIAN_POINT('Ctrl Pts',(-8.14703538592992,1.21601760624665,17.0989990289619));
#30971=CARTESIAN_POINT('Ctrl Pts',(-8.75457747423087,1.24035201730987,17.122152949811));
#30972=CARTESIAN_POINT('Ctrl Pts',(-9.30341679390951,0.978674783003138,
17.14530687066));
#30973=CARTESIAN_POINT('Ctrl Pts',(-9.66699689558182,0.491325749557319,
17.1684607915091));
#30974=CARTESIAN_POINT('Ctrl Pts',(-9.76148033787767,-0.10931754119764,
17.1916147123582));
#30975=CARTESIAN_POINT('Ctrl Pts',(-9.56507989669121,-0.68475363956845,
17.2147686332073));
#30976=CARTESIAN_POINT('Ctrl Pts',(-9.12308418289996,-1.1022924873685,17.2379225540564));
#30977=CARTESIAN_POINT('Ctrl Pts',(-8.53741084518169,-1.26565584737736,
17.2610764749055));
#30978=CARTESIAN_POINT('Ctrl Pts',(-7.94311359864215,-1.13717035634921,
17.2842303957546));
#30979=CARTESIAN_POINT('Ctrl Pts',(-7.47722268493459,-0.746471406749234,
17.3073843166036));
#30980=CARTESIAN_POINT('Ctrl Pts',(-7.24718561960605,-0.183633649692887,
17.3305382374527));
#30981=CARTESIAN_POINT('Ctrl Pts',(-7.3060079723258,0.421518864292242,17.3536921583018));
#30982=CARTESIAN_POINT('Ctrl Pts',(-7.64021327215519,0.929515170005604,
17.3768460791509));
#30983=CARTESIAN_POINT('Ctrl Pts',(-7.99510874416169,1.12516550422184,17.3922820263836));
#30984=CARTESIAN_POINT('Ctrl Pts',(-8.18521110449555,1.17604951161381,17.4));
#30985=CARTESIAN_POINT('Ctrl Pts',(-8.18521110449555,1.17604951161381,17.4));
#30986=CARTESIAN_POINT('Ctrl Pts',(-8.13719933141137,1.1596386310925,17.4));
#30987=CARTESIAN_POINT('Ctrl Pts',(-8.09039173307286,1.14022110224332,17.4));
#30988=CARTESIAN_POINT('Ctrl Pts',(-8.04502617402981,1.11798780897205,17.4));
#30989=CARTESIAN_POINT('Ctrl Pts',(-7.99968282249027,1.09576539941849,17.4));
#30990=CARTESIAN_POINT('Ctrl Pts',(-7.95577920066712,1.07072928126397,17.4));
#30991=CARTESIAN_POINT('Ctrl Pts',(-7.91358006184999,1.04302582262482,17.4));
#30992=CARTESIAN_POINT('Ctrl Pts',(-7.87480130346833,1.01756782137131,17.4));
#30993=CARTESIAN_POINT('Ctrl Pts',(-7.83746169262404,0.98985647985361,17.4));
#30994=CARTESIAN_POINT('Ctrl Pts',(-7.80179671782517,0.959979848904726,
17.4));
#30995=CARTESIAN_POINT('Ctrl Pts',(-7.79470096127184,0.954035717413182,
17.4));
#30996=CARTESIAN_POINT('Ctrl Pts',(-7.78766995121509,0.948004356872779,
17.4));
#30997=CARTESIAN_POINT('Ctrl Pts',(-7.78071104889818,0.941891074987019,
17.4));
#30998=CARTESIAN_POINT('Ctrl Pts',(-7.75269283864155,0.917277535461247,
17.4));
#30999=CARTESIAN_POINT('Ctrl Pts',(-7.72591217218802,0.89139923448771,17.4));
#31000=CARTESIAN_POINT('Ctrl Pts',(-7.70047050940558,0.864320484202139,
17.4));
#31001=CARTESIAN_POINT('Ctrl Pts',(-7.66652610990813,0.828191873999045,
17.4));
#31002=CARTESIAN_POINT('Ctrl Pts',(-7.63496332880565,0.789926935722668,
17.4));
#31003=CARTESIAN_POINT('Ctrl Pts',(-7.60593193600345,0.749791972759857,
17.4));
#31004=CARTESIAN_POINT('Ctrl Pts',(-7.58573671276234,0.721872728845864,
17.4));
#31005=CARTESIAN_POINT('Ctrl Pts',(-7.56676729894315,0.693047838849524,
17.4));
#31006=CARTESIAN_POINT('Ctrl Pts',(-7.54908781912516,0.6634012006176,17.4));
#31007=CARTESIAN_POINT('Ctrl Pts',(-7.53965707725517,0.647586833036838,
17.4));
#31008=CARTESIAN_POINT('Ctrl Pts',(-7.53059358194979,0.631538581376815,
17.4));
#31009=CARTESIAN_POINT('Ctrl Pts',(-7.52190851593401,0.615268925347433,
17.4));
#31010=CARTESIAN_POINT('Ctrl Pts',(-7.5174887289744,0.606989378200016,17.4));
#31011=CARTESIAN_POINT('Ctrl Pts',(-7.51316696210323,0.598652491346504,
17.4));
#31012=CARTESIAN_POINT('Ctrl Pts',(-7.5089447953144,0.590259903970057,17.4));
#31013=CARTESIAN_POINT('Ctrl Pts',(-7.50442274498419,0.58127122483559,17.4));
#31014=CARTESIAN_POINT('Ctrl Pts',(-7.50001831617906,0.572225198393919,
17.4));
#31015=CARTESIAN_POINT('Ctrl Pts',(-7.49573624060671,0.563131408297169,
17.4));
#31016=CARTESIAN_POINT('Ctrl Pts',(-7.47506504458002,0.51923224899006,17.4));
#31017=CARTESIAN_POINT('Ctrl Pts',(-7.45721461446443,0.474168760407469,
17.4));
#31018=CARTESIAN_POINT('Ctrl Pts',(-7.44233244334752,0.428188460522925,
17.4));
#31019=CARTESIAN_POINT('Ctrl Pts',(-7.43702154871991,0.411779797719997,
17.4));
#31020=CARTESIAN_POINT('Ctrl Pts',(-7.4320891210697,0.395254227754963,17.4));
#31021=CARTESIAN_POINT('Ctrl Pts',(-7.42754343894325,0.378622633207859,
17.4));
#31022=CARTESIAN_POINT('Ctrl Pts',(-7.41562263365724,0.335007176896464,
17.4));
#31023=CARTESIAN_POINT('Ctrl Pts',(-7.40635878862766,0.290662257255706,
17.4));
#31024=CARTESIAN_POINT('Ctrl Pts',(-7.39978211476199,0.24583513299177,17.4));
#31025=CARTESIAN_POINT('Ctrl Pts',(-7.3970185212721,0.22699826327361,17.4));
#31026=CARTESIAN_POINT('Ctrl Pts',(-7.39472989763131,0.208076295947074,
17.4));
#31027=CARTESIAN_POINT('Ctrl Pts',(-7.39292054511252,0.189088017812139,
17.4));
#31028=CARTESIAN_POINT('Ctrl Pts',(-7.39203065715885,0.179749074849041,
17.4));
#31029=CARTESIAN_POINT('Ctrl Pts',(-7.39125658497907,0.170392126906475,
17.4));
#31030=CARTESIAN_POINT('Ctrl Pts',(-7.3905993784452,0.161025711582129,17.4));
#31031=CARTESIAN_POINT('Ctrl Pts',(-7.38726338063351,0.113481538761262,
17.4));
#31032=CARTESIAN_POINT('Ctrl Pts',(-7.38694615050342,0.0658811286412803,
17.4));
#31033=CARTESIAN_POINT('Ctrl Pts',(-7.3896450240632,0.0185133652028824,
17.4));
#31034=CARTESIAN_POINT('Ctrl Pts',(-7.39231331845235,-0.0283177050974028,
17.4));
#31035=CARTESIAN_POINT('Ctrl Pts',(-7.39792993724915,-0.0749224438741415,
17.4));
#31036=CARTESIAN_POINT('Ctrl Pts',(-7.40654177913599,-0.121012609291369,
17.4));
#31037=CARTESIAN_POINT('Ctrl Pts',(-7.40892366435284,-0.133760344920039,
17.4));
#31038=CARTESIAN_POINT('Ctrl Pts',(-7.41153496349064,-0.146468610849955,
17.4));
#31039=CARTESIAN_POINT('Ctrl Pts',(-7.41437732095262,-0.159131017394972,
17.4));
#31040=CARTESIAN_POINT('Ctrl Pts',(-7.41931603486849,-0.181132473668076,
17.4));
#31041=CARTESIAN_POINT('Ctrl Pts',(-7.4249522210655,-0.202995576069695,
17.4));
#31042=CARTESIAN_POINT('Ctrl Pts',(-7.4312759353939,-0.224688518418572,
17.4));
#31043=CARTESIAN_POINT('Ctrl Pts',(-7.43448590379059,-0.235700030918177,
17.4));
#31044=CARTESIAN_POINT('Ctrl Pts',(-7.43787305827033,-0.246667672522508,
17.4));
#31045=CARTESIAN_POINT('Ctrl Pts',(-7.44143629568122,-0.257587102480944,
17.4));
#31046=CARTESIAN_POINT('Ctrl Pts',(-7.4446648798304,-0.267480997951973,
17.4));
#31047=CARTESIAN_POINT('Ctrl Pts',(-7.44803542440217,-0.277327204922127,
17.4));
#31048=CARTESIAN_POINT('Ctrl Pts',(-7.45154495609234,-0.287118681769737,
17.4));
#31049=CARTESIAN_POINT('Ctrl Pts',(-7.46731965368996,-0.331129564115665,
17.4));
#31050=CARTESIAN_POINT('Ctrl Pts',(-7.48590775064078,-0.374064115176777,
17.4));
#31051=CARTESIAN_POINT('Ctrl Pts',(-7.50719055019682,-0.415647717031525,
17.4));
#31052=CARTESIAN_POINT('Ctrl Pts',(-7.51904291434652,-0.438805572300566,
17.4));
#31053=CARTESIAN_POINT('Ctrl Pts',(-7.53173179424408,-0.461543974053204,
17.4));
#31054=CARTESIAN_POINT('Ctrl Pts',(-7.54524198733332,-0.48381081567099,
17.4));
#31055=CARTESIAN_POINT('Ctrl Pts',(-7.55097571485935,-0.493260865855931,
17.4));
#31056=CARTESIAN_POINT('Ctrl Pts',(-7.55685683761236,-0.502624737244181,
17.4));
#31057=CARTESIAN_POINT('Ctrl Pts',(-7.56287734293596,-0.511888319657218,
17.4));
#31058=CARTESIAN_POINT('Ctrl Pts',(-7.58817043839211,-0.550806095100506,
17.4));
#31059=CARTESIAN_POINT('Ctrl Pts',(-7.61595063019034,-0.588007205459175,
17.4));
#31060=CARTESIAN_POINT('Ctrl Pts',(-7.64611656408827,-0.623204427033219,
17.4));
#31061=CARTESIAN_POINT('Ctrl Pts',(-7.66532319320885,-0.645614473515954,
17.4));
#31062=CARTESIAN_POINT('Ctrl Pts',(-7.68549786483987,-0.667211399547439,
17.4));
#31063=CARTESIAN_POINT('Ctrl Pts',(-7.70658083841843,-0.687941007615962,
17.4));
#31064=CARTESIAN_POINT('Ctrl Pts',(-7.70661869325987,-0.687936125025659,
16.2));
#31065=CARTESIAN_POINT('Ctrl Pts',(-7.67409819941258,-0.655901613373747,
16.2));
#31066=CARTESIAN_POINT('Ctrl Pts',(-7.64381371410258,-0.621807353051285,
16.2));
#31067=CARTESIAN_POINT('Ctrl Pts',(-7.61585565959385,-0.585952756227217,
16.2));
#31068=CARTESIAN_POINT('Ctrl Pts',(-7.58749905195372,-0.549587037935981,
16.2));
#31069=CARTESIAN_POINT('Ctrl Pts',(-7.56153494829612,-0.511409649371158,
16.2));
#31070=CARTESIAN_POINT('Ctrl Pts',(-7.53808804236644,-0.471687753089119,
16.2));
#31071=CARTESIAN_POINT('Ctrl Pts',(-7.51732645863979,-0.436515117607317,
16.2));
#31072=CARTESIAN_POINT('Ctrl Pts',(-7.4985386214165,-0.400130432937881,
16.2));
#31073=CARTESIAN_POINT('Ctrl Pts',(-7.48183756845935,-0.362697997620638,
16.2));
#31074=CARTESIAN_POINT('Ctrl Pts',(-7.47711052305992,-0.352103167365936,
16.2));
#31075=CARTESIAN_POINT('Ctrl Pts',(-7.47254949524406,-0.341420594140401,
16.2));
#31076=CARTESIAN_POINT('Ctrl Pts',(-7.46816743540603,-0.330679560210348,
16.2));
#31077=CARTESIAN_POINT('Ctrl Pts',(-7.45706730558176,-0.303471608818189,
16.2));
#31078=CARTESIAN_POINT('Ctrl Pts',(-7.44710097243911,-0.275859205740836,
16.2));
#31079=CARTESIAN_POINT('Ctrl Pts',(-7.43829583898931,-0.247910972255057,
16.2));
#31080=CARTESIAN_POINT('Ctrl Pts',(-7.42417626257798,-0.203094250224204,
16.2));
#31081=CARTESIAN_POINT('Ctrl Pts',(-7.41303986581868,-0.157415105126112,
16.2));
#31082=CARTESIAN_POINT('Ctrl Pts',(-7.40485132275059,-0.111177022987818,
16.2));
#31083=CARTESIAN_POINT('Ctrl Pts',(-7.39906463642413,-0.0785014572068798,
16.2));
#31084=CARTESIAN_POINT('Ctrl Pts',(-7.39475106098134,-0.0455460201930134,
16.2));
#31085=CARTESIAN_POINT('Ctrl Pts',(-7.3919127668216,-0.0124120211671536,
16.2));
#31086=CARTESIAN_POINT('Ctrl Pts',(-7.39015412848058,0.0081181697852479,
16.2));
#31087=CARTESIAN_POINT('Ctrl Pts',(-7.38896211845984,0.0287169905616347,
16.2));
#31088=CARTESIAN_POINT('Ctrl Pts',(-7.38833968108958,0.049360700311489,
16.2));
#31089=CARTESIAN_POINT('Ctrl Pts',(-7.38797753653769,0.0613715585501746,
16.2));
#31090=CARTESIAN_POINT('Ctrl Pts',(-7.38780840935154,0.0734020382686694,
16.2));
#31091=CARTESIAN_POINT('Ctrl Pts',(-7.38783261787483,0.0854186284205357,
16.2));
#31092=CARTESIAN_POINT('Ctrl Pts',(-7.38793000681716,0.133760404211766,
16.2));
#31093=CARTESIAN_POINT('Ctrl Pts',(-7.39114764392613,0.181958557559603,
16.2));
#31094=CARTESIAN_POINT('Ctrl Pts',(-7.3974533166152,0.229702110452317,16.2));
#31095=CARTESIAN_POINT('Ctrl Pts',(-7.39993002168277,0.248454542623161,
16.2));
#31096=CARTESIAN_POINT('Ctrl Pts',(-7.40288366457642,0.267137030119369,
16.2));
#31097=CARTESIAN_POINT('Ctrl Pts',(-7.40631442558066,0.285731222217819,
16.2));
#31098=CARTESIAN_POINT('Ctrl Pts',(-7.41475452038151,0.33147522591313,16.2));
#31099=CARTESIAN_POINT('Ctrl Pts',(-7.42607900308179,0.376685278391262,
16.2));
#31100=CARTESIAN_POINT('Ctrl Pts',(-7.44015772007498,0.42113138571071,16.2));
#31101=CARTESIAN_POINT('Ctrl Pts',(-7.44619795546194,0.440200236258183,
16.2));
#31102=CARTESIAN_POINT('Ctrl Pts',(-7.45274573481429,0.459128399707979,
16.2));
#31103=CARTESIAN_POINT('Ctrl Pts',(-7.45979327769237,0.477897135727449,
16.2));
#31104=CARTESIAN_POINT('Ctrl Pts',(-7.4642421136194,0.489745098705874,16.2));
#31105=CARTESIAN_POINT('Ctrl Pts',(-7.468892265084,0.501534238264903,16.2));
#31106=CARTESIAN_POINT('Ctrl Pts',(-7.47372969293921,0.513231143469178,
16.2));
#31107=CARTESIAN_POINT('Ctrl Pts',(-7.49246801605267,0.55854042677133,16.2));
#31108=CARTESIAN_POINT('Ctrl Pts',(-7.51403710348823,0.602539209890798,
16.2));
#31109=CARTESIAN_POINT('Ctrl Pts',(-7.53825701358138,0.64497355101848,16.2));
#31110=CARTESIAN_POINT('Ctrl Pts',(-7.56269796362399,0.6877951637992,16.2));
#31111=CARTESIAN_POINT('Ctrl Pts',(-7.58983866618497,0.729024731678887,
16.2));
#31112=CARTESIAN_POINT('Ctrl Pts',(-7.61954508460314,0.768389575096334,
16.2));
#31113=CARTESIAN_POINT('Ctrl Pts',(-7.62494291098869,0.775542392627911,
16.2));
#31114=CARTESIAN_POINT('Ctrl Pts',(-7.63042557616055,0.782633586115029,
16.2));
#31115=CARTESIAN_POINT('Ctrl Pts',(-7.63599244107805,0.789661434383682,
16.2));
#31116=CARTESIAN_POINT('Ctrl Pts',(-7.65116980668403,0.808821989593387,
16.2));
#31117=CARTESIAN_POINT('Ctrl Pts',(-7.66697286226321,0.827511837810756,
16.2));
#31118=CARTESIAN_POINT('Ctrl Pts',(-7.68337336577547,0.845710316113916,
16.2));
#31119=CARTESIAN_POINT('Ctrl Pts',(-7.69112549719668,0.854312307837324,
16.2));
#31120=CARTESIAN_POINT('Ctrl Pts',(-7.69901114804083,0.862804487247497,
16.2));
#31121=CARTESIAN_POINT('Ctrl Pts',(-7.70702751694813,0.871184505187608,
16.2));
#31122=CARTESIAN_POINT('Ctrl Pts',(-7.71445522191538,0.878949155442497,
16.2));
#31123=CARTESIAN_POINT('Ctrl Pts',(-7.72198944448574,0.886611472889222,
16.2));
#31124=CARTESIAN_POINT('Ctrl Pts',(-7.72962359681997,0.894166271565807,
16.2));
#31125=CARTESIAN_POINT('Ctrl Pts',(-7.76528162277488,0.929453648015724,
16.2));
#31126=CARTESIAN_POINT('Ctrl Pts',(-7.80314159744981,0.962424156726079,
16.2));
#31127=CARTESIAN_POINT('Ctrl Pts',(-7.8429321675271,0.99292226510897,16.2));
#31128=CARTESIAN_POINT('Ctrl Pts',(-7.86517997576319,1.00997444771274,16.2));
#31129=CARTESIAN_POINT('Ctrl Pts',(-7.8880321474545,1.02625321846037,16.2));
#31130=CARTESIAN_POINT('Ctrl Pts',(-7.9114465947083,1.04172678059142,16.2));
#31131=CARTESIAN_POINT('Ctrl Pts',(-7.92363396469123,1.04978086893273,16.2));
#31132=CARTESIAN_POINT('Ctrl Pts',(-7.93597595875067,1.05761787570908,16.2));
#31133=CARTESIAN_POINT('Ctrl Pts',(-7.94844653765927,1.06522111773372,16.2));
#31134=CARTESIAN_POINT('Ctrl Pts',(-7.99400655072966,1.09299880219879,16.2));
#31135=CARTESIAN_POINT('Ctrl Pts',(-8.04133366721399,1.11769730011503,16.2));
#31136=CARTESIAN_POINT('Ctrl Pts',(-8.09012860071083,1.13911605908712,16.2));
#31137=CARTESIAN_POINT('Ctrl Pts',(-8.12124378896121,1.15277421311553,16.2));
#31138=CARTESIAN_POINT('Ctrl Pts',(-8.15295679384449,1.16509791067328,16.2));
#31139=CARTESIAN_POINT('Ctrl Pts',(-8.18517792975413,1.17607879646049,16.2));
#31140=CARTESIAN_POINT('Ctrl Pts',(-9.55016499124735,-1.36965953006496E-5,
16.6841069671524));
#31141=CARTESIAN_POINT('Ctrl Pts',(-9.55006230523617,0.154119242885846,
16.6770974504288));
#31142=CARTESIAN_POINT('Ctrl Pts',(-9.51567286587192,0.308296531891891,
16.6700879337053));
#31143=CARTESIAN_POINT('Ctrl Pts',(-9.4499660772856,0.447714115625669,16.6630784169817));
#31144=CARTESIAN_POINT('Ctrl Pts',(-9.37761825635498,0.601222734743451,
16.6553604433654));
#31145=CARTESIAN_POINT('Ctrl Pts',(-9.26730263640673,0.736837325878114,
16.647642469749));
#31146=CARTESIAN_POINT('Ctrl Pts',(-9.13173800779262,0.838922265066044,
16.6399244961327));
#31147=CARTESIAN_POINT('Ctrl Pts',(-8.99617337917851,0.941007204253974,
16.6322065225163));
#31148=CARTESIAN_POINT('Ctrl Pts',(-8.83535974189854,1.00956249149517,16.6244885488999));
#31149=CARTESIAN_POINT('Ctrl Pts',(-8.66783803278417,1.03668407535848,16.6167705752836));
#31150=CARTESIAN_POINT('Ctrl Pts',(-8.5003163236698,1.06380565922179,16.6090526016672));
#31151=CARTESIAN_POINT('Ctrl Pts',(-8.32608654272104,1.04949353970721,16.6013346280508));
#31152=CARTESIAN_POINT('Ctrl Pts',(-8.16523643504245,0.995397826415959,
16.5936166544345));
#31153=CARTESIAN_POINT('Ctrl Pts',(-8.00438632736387,0.941302113124703,
16.5858986808181));
#31154=CARTESIAN_POINT('Ctrl Pts',(-7.85691589295546,0.847422806056768,
16.5781807072018));
#31155=CARTESIAN_POINT('Ctrl Pts',(-7.73982767006045,0.724583677870246,
16.5704627335854));
#31156=CARTESIAN_POINT('Ctrl Pts',(-7.62273944716545,0.601744549683724,
16.562744759969));
#31157=CARTESIAN_POINT('Ctrl Pts',(-7.53603343578385,0.449945600378615,
16.5550267863527));
#31158=CARTESIAN_POINT('Ctrl Pts',(-7.4897063667997,0.286688423011718,16.5473088127363));
#31159=CARTESIAN_POINT('Ctrl Pts',(-7.44337929781555,0.12343124564482,16.5395908391199));
#31160=CARTESIAN_POINT('Ctrl Pts',(-7.43743117122886,-0.0512841597838649,
16.5318728655036));
#31161=CARTESIAN_POINT('Ctrl Pts',(-7.47254777397841,-0.217314059761718,
16.5241548918872));
#31162=CARTESIAN_POINT('Ctrl Pts',(-7.50766437672797,-0.383343959739573,
16.5164369182709));
#31163=CARTESIAN_POINT('Ctrl Pts',(-7.58384570881378,-0.540688354266594,
16.5087189446545));
#31164=CARTESIAN_POINT('Ctrl Pts',(-7.69230847670872,-0.67120628810507,
16.5010009710381));
#31165=CARTESIAN_POINT('Ctrl Pts',(-7.80077124460366,-0.801724221943545,
16.4932829974218));
#31166=CARTESIAN_POINT('Ctrl Pts',(-7.94151544830774,-0.905415695093475,
16.4855650238054));
#31167=CARTESIAN_POINT('Ctrl Pts',(-8.09831404897755,-0.970325652253155,
16.477847050189));
#31168=CARTESIAN_POINT('Ctrl Pts',(-8.25511264964736,-1.03523560941283,
16.4701290765727));
#31169=CARTESIAN_POINT('Ctrl Pts',(-8.4279656472829,-1.06136405058227,16.4624111029563));
#31170=CARTESIAN_POINT('Ctrl Pts',(-8.59694402900981,-1.04569849353872,
16.45469312934));
#31171=CARTESIAN_POINT('Ctrl Pts',(-8.76592241073672,-1.03003293649518,
16.4469751557236));
#31172=CARTESIAN_POINT('Ctrl Pts',(-8.93102617655499,-0.972573381238667,
16.4392571821072));
#31173=CARTESIAN_POINT('Ctrl Pts',(-9.07321976852969,-0.879944634656233,
16.4315392084909));
#31174=CARTESIAN_POINT('Ctrl Pts',(-9.21541336050439,-0.7873158880738,16.4238212348745));
#31175=CARTESIAN_POINT('Ctrl Pts',(-9.33469677863551,-0.659517950165448,
16.4161032612582));
#31176=CARTESIAN_POINT('Ctrl Pts',(-9.41731727848406,-0.511285155476193,
16.4083852876418));
#31177=CARTESIAN_POINT('Ctrl Pts',(-9.49993777833262,-0.363052360786937,
16.4006673140254));
#31178=CARTESIAN_POINT('Ctrl Pts',(-9.54589535989859,-0.194384709316778,
16.3929493404091));
#31179=CARTESIAN_POINT('Ctrl Pts',(-9.54989139919407,-0.0247288185109309,
16.3852313667927));
#31180=CARTESIAN_POINT('Ctrl Pts',(-9.55008545467072,-0.0164899969375102,
16.3848565669126));
#31181=CARTESIAN_POINT('Ctrl Pts',(-9.55018055377881,-0.00824884483545272,
16.3844817670325));
#31182=CARTESIAN_POINT('Ctrl Pts',(-9.55017719779692,-7.61530804432864E-6,
16.3841069671524));
#31183=CARTESIAN_POINT('Ctrl Pts',(-8.81478889550445,1.17604951161381,16.2));
#31184=CARTESIAN_POINT('Ctrl Pts',(-9.00489125583831,1.12516550422184,16.2077179736164));
#31185=CARTESIAN_POINT('Ctrl Pts',(-9.35978667802179,0.929514905730451,
16.2231539208491));
#31186=CARTESIAN_POINT('Ctrl Pts',(-9.69399203697644,0.421518824488713,
16.2463078416982));
#31187=CARTESIAN_POINT('Ctrl Pts',(-9.75281439556121,-0.18363371105277,
16.2694617625473));
#31188=CARTESIAN_POINT('Ctrl Pts',(-9.52277733259636,-0.746471423726082,
16.2926156833963));
#31189=CARTESIAN_POINT('Ctrl Pts',(-9.05688641176464,-1.13717038838356,
16.3157696042454));
#31190=CARTESIAN_POINT('Ctrl Pts',(-8.46258915349396,-1.26565587137657,
16.3389235250945));
#31191=CARTESIAN_POINT('Ctrl Pts',(-7.87691580481983,-1.10229251092252,
16.3620774459436));
#31192=CARTESIAN_POINT('Ctrl Pts',(-7.43492008199845,-0.684753652714294,
16.3852313667927));
#31193=CARTESIAN_POINT('Ctrl Pts',(-7.23851963711968,-0.109317543695422,
16.4083852876418));
#31194=CARTESIAN_POINT('Ctrl Pts',(-7.33300308119116,0.491325759444495,
16.4315392084909));
#31195=CARTESIAN_POINT('Ctrl Pts',(-7.69658319014803,0.978674802377791,
16.45469312934));
#31196=CARTESIAN_POINT('Ctrl Pts',(-8.24542252070005,1.24035204198393,16.477847050189));
#31197=CARTESIAN_POINT('Ctrl Pts',(-8.85296462108838,1.21601763039105,16.5010009710381));
#31198=CARTESIAN_POINT('Ctrl Pts',(-9.37911693472505,0.911282783877038,
16.5241548918872));
#31199=CARTESIAN_POINT('Ctrl Pts',(-9.702554450806,0.396416055432127,16.5473088127363));
#31200=CARTESIAN_POINT('Ctrl Pts',(-9.74869600773439,-0.209859901037287,
16.5704627335854));
#31201=CARTESIAN_POINT('Ctrl Pts',(-9.50690186140351,-0.767744448476627,
16.5936166544345));
#31202=CARTESIAN_POINT('Ctrl Pts',(-9.0329271106457,-1.14859548666069,16.6167705752836));
#31203=CARTESIAN_POINT('Ctrl Pts',(-8.4360651710595,-1.26459291262403,16.6399244961327));
#31204=CARTESIAN_POINT('Ctrl Pts',(-7.85394590693938,-1.08898898337596,
16.6630784169817));
#31205=CARTESIAN_POINT('Ctrl Pts',(-7.42079968165148,-0.662276052675294,
16.6862323378308));
#31206=CARTESIAN_POINT('Ctrl Pts',(-7.23650529822705,-0.0828494758703863,
16.7093862586799));
#31207=CARTESIAN_POINT('Ctrl Pts',(-7.34355903464176,0.515681287920065,
16.732540179529));
#31208=CARTESIAN_POINT('Ctrl Pts',(-7.71727546501759,0.995301562040781,
16.7556941003781));
#31209=CARTESIAN_POINT('Ctrl Pts',(-8.27147964995585,1.24541613394172,16.7788480212272));
#31210=CARTESIAN_POINT('Ctrl Pts',(-8.8783781392237,1.20835130687373,16.8020019420763));
#31211=CARTESIAN_POINT('Ctrl Pts',(-9.39802674980115,0.892653826355733,
16.8251558629254));
#31212=CARTESIAN_POINT('Ctrl Pts',(-9.71060017061972,0.371120093718434,
16.8483097837744));
#31213=CARTESIAN_POINT('Ctrl Pts',(-9.74402237449611,-0.235989891349228,
16.8714637046235));
#31214=CARTESIAN_POINT('Ctrl Pts',(-9.49058656515595,-0.788683177200059,
16.8946176254726));
#31215=CARTESIAN_POINT('Ctrl Pts',(-9.0087322805331,-1.15951471047599,16.9177715463217));
#31216=CARTESIAN_POINT('Ctrl Pts',(-8.40956987168007,-1.26297477764059,
16.9409254671708));
#31217=CARTESIAN_POINT('Ctrl Pts',(-7.83125966571002,-1.07520661380189,
16.9640793880199));
#31218=CARTESIAN_POINT('Ctrl Pts',(-7.40715369881707,-0.639507512896534,
16.987233308869));
#31219=CARTESIAN_POINT('Ctrl Pts',(-7.23504618881006,-0.0563449432224961,
17.010387229718));
#31220=CARTESIAN_POINT('Ctrl Pts',(-7.35462325340267,0.539810156841002,
17.0335411505671));
#31221=CARTESIAN_POINT('Ctrl Pts',(-7.73831172357029,1.01149091274223,17.0566950714162));
#31222=CARTESIAN_POINT('Ctrl Pts',(-8.29763721617962,1.24993287858306,17.0798489922653));
#31223=CARTESIAN_POINT('Ctrl Pts',(-8.90362536310944,1.20015393300998,17.1030029131144));
#31224=CARTESIAN_POINT('Ctrl Pts',(-9.41654189659505,0.873632559821981,
17.1261568339635));
#31225=CARTESIAN_POINT('Ctrl Pts',(-9.71811384875226,0.34566102996382,17.1493107548126));
#31226=CARTESIAN_POINT('Ctrl Pts',(-9.73880201233004,-0.262016166215173,
17.1724646756617));
#31227=CARTESIAN_POINT('Ctrl Pts',(-9.47383591978867,-0.809275294625564,
17.1956185965107));
#31228=CARTESIAN_POINT('Ctrl Pts',(-8.98431387179416,-1.16992433712962,
17.2187725173598));
#31229=CARTESIAN_POINT('Ctrl Pts',(-8.38311431128619,-1.26080160014802,
17.2419264382089));
#31230=CARTESIAN_POINT('Ctrl Pts',(-7.80886733385048,-1.06095167099359,
17.265080359058));
#31231=CARTESIAN_POINT('Ctrl Pts',(-7.39398798803169,-0.616457995871644,
17.2882342799071));
#31232=CARTESIAN_POINT('Ctrl Pts',(-7.23414304365684,-0.0298154777491022,
17.3113882007562));
#31233=CARTESIAN_POINT('Ctrl Pts',(-7.36619075960647,0.563701428344329,
17.3345421216053));
#31234=CARTESIAN_POINT('Ctrl Pts',(-7.75968288434054,1.02723654746506,17.3576960424544));
#31235=CARTESIAN_POINT('Ctrl Pts',(-8.32388323581996,1.25389866145525,17.3808499633034));
#31236=CARTESIAN_POINT('Ctrl Pts',(-8.92869568375729,1.19143319965512,17.4040038841525));
#31237=CARTESIAN_POINT('Ctrl Pts',(-9.43465110964391,0.854220435720086,
17.4271578050016));
#31238=CARTESIAN_POINT('Ctrl Pts',(-9.72509133177006,0.320072386474311,
17.4503117258507));
#31239=CARTESIAN_POINT('Ctrl Pts',(-9.73301103905973,-0.287949421315032,
17.4734656466998));
#31240=CARTESIAN_POINT('Ctrl Pts',(-9.54874216054249,-0.648885562185997,
17.4889015939325));
#31241=CARTESIAN_POINT('Ctrl Pts',(-9.41981913331184,-0.797569598526339,
17.4966195675489));
#31242=CARTESIAN_POINT('Ctrl Pts',(-8.80036532666174,1.12216314098434,16.1677934774837));
#31243=CARTESIAN_POINT('Ctrl Pts',(-8.9817572320825,1.0736106293792,16.1755114511001));
#31244=CARTESIAN_POINT('Ctrl Pts',(-9.32039141180499,0.886924705044866,
16.1909473983328));
#31245=CARTESIAN_POINT('Ctrl Pts',(-9.63928354316068,0.402204910083416,
16.2141013191819));
#31246=CARTESIAN_POINT('Ctrl Pts',(-9.69541067217841,-0.175219648450697,
16.237255240031));
#31247=CARTESIAN_POINT('Ctrl Pts',(-9.47591386479892,-0.712268241456979,
16.26040916088));
#31248=CARTESIAN_POINT('Ctrl Pts',(-9.03136997960212,-1.08506545197385,
16.2835630817291));
#31249=CARTESIAN_POINT('Ctrl Pts',(-8.46430331154639,-1.20766375395221,
16.3067170025782));
#31250=CARTESIAN_POINT('Ctrl Pts',(-7.90546540714803,-1.05178567239311,
16.3298709234273));
#31251=CARTESIAN_POINT('Ctrl Pts',(-7.48372184641795,-0.653378367272938,
16.3530248442764));
#31252=CARTESIAN_POINT('Ctrl Pts',(-7.29632043351871,-0.10430863410641,
16.3761787651255));
#31253=CARTESIAN_POINT('Ctrl Pts',(-7.38647466369631,0.468813304218946,
16.3993326859746));
#31254=CARTESIAN_POINT('Ctrl Pts',(-7.73339559945402,0.93383210434011,16.4224866068237));
#31255=CARTESIAN_POINT('Ctrl Pts',(-8.25708721361307,1.18351934133202,16.4456405276728));
#31256=CARTESIAN_POINT('Ctrl Pts',(-8.83679184757567,1.1602999279677,16.4687944485218));
#31257=CARTESIAN_POINT('Ctrl Pts',(-9.33883595972916,0.869527975635269,
16.4919483693709));
#31258=CARTESIAN_POINT('Ctrl Pts',(-9.6474536287757,0.378252345251951,16.51510229022));
#31259=CARTESIAN_POINT('Ctrl Pts',(-9.69148098811842,-0.200244159271414,
16.5382562110691));
#31260=CARTESIAN_POINT('Ctrl Pts',(-9.46076580475344,-0.732566540156623,
16.5614101319182));
#31261=CARTESIAN_POINT('Ctrl Pts',(-9.00850848921934,-1.09596705436568,
16.5845640527673));
#31262=CARTESIAN_POINT('Ctrl Pts',(-8.43899465307059,-1.20664949977268,
16.6077179736164));
#31263=CARTESIAN_POINT('Ctrl Pts',(-7.88354798573076,-1.03909171001279,
16.6308718944654));
#31264=CARTESIAN_POINT('Ctrl Pts',(-7.47024844019752,-0.631930686701274,
16.6540258153145));
#31265=CARTESIAN_POINT('Ctrl Pts',(-7.29439839126077,-0.0790533282429932,
16.6771797361636));
#31266=CARTESIAN_POINT('Ctrl Pts',(-7.39654694531645,0.492052866894308,
16.7003336570127));
#31267=CARTESIAN_POINT('Ctrl Pts',(-7.75313975812458,0.949697028957279,
16.7234875778618));
#31268=CARTESIAN_POINT('Ctrl Pts',(-8.28195041003631,1.18835139753498,16.7466414987109));
#31269=CARTESIAN_POINT('Ctrl Pts',(-8.86104092302068,1.15298487397291,16.76979541956));
#31270=CARTESIAN_POINT('Ctrl Pts',(-9.3568793305836,0.851752593494524,16.7929493404091));
#31271=CARTESIAN_POINT('Ctrl Pts',(-9.6551306951989,0.354115439815118,16.8161032612581));
#31272=CARTESIAN_POINT('Ctrl Pts',(-9.68702149988882,-0.225176878270719,
16.8392571821072));
#31273=CARTESIAN_POINT('Ctrl Pts',(-9.44519807235574,-0.752545860211153,
16.8624111029563));
#31274=CARTESIAN_POINT('Ctrl Pts',(-8.98542226173774,-1.10638596136976,
16.8855650238054));
#31275=CARTESIAN_POINT('Ctrl Pts',(-8.41371336339756,-1.20510550743424,
16.9087189446545));
#31276=CARTESIAN_POINT('Ctrl Pts',(-7.8619012238694,-1.0259408460579,16.9318728655036));
#31277=CARTESIAN_POINT('Ctrl Pts',(-7.45722771376716,-0.610205397194798,
16.9550267863527));
#31278=CARTESIAN_POINT('Ctrl Pts',(-7.2930061379668,-0.0537632283681462,
16.9781807072018));
#31279=CARTESIAN_POINT('Ctrl Pts',(-7.4071042036246,0.515076155513817,17.0013346280508));
#31280=CARTESIAN_POINT('Ctrl Pts',(-7.77321213920967,0.965144586610446,
17.0244885488999));
#31281=CARTESIAN_POINT('Ctrl Pts',(-8.30690944142428,1.19266118577408,17.047642469749));
#31282=CARTESIAN_POINT('Ctrl Pts',(-8.88513132378781,1.14516310226012,17.0707963905981));
#31283=CARTESIAN_POINT('Ctrl Pts',(-9.37454611678337,0.833602877867565,
17.0939503114472));
#31284=CARTESIAN_POINT('Ctrl Pts',(-9.66230009799215,0.329822905642644,
17.1171042322963));
#31285=CARTESIAN_POINT('Ctrl Pts',(-9.68204033374956,-0.250010634046539,
17.1402581531454));
#31286=CARTESIAN_POINT('Ctrl Pts',(-9.42921493845428,-0.772194450633179,
17.1634120739945));
#31287=CARTESIAN_POINT('Ctrl Pts',(-8.96212269996102,-1.11631862085965,
17.1865659948435));
#31288=CARTESIAN_POINT('Ctrl Pts',(-8.38846999187711,-1.20303190453157,
17.2097199156926));
#31289=CARTESIAN_POINT('Ctrl Pts',(-7.84053490450502,-1.01233906208678,
17.2328738365417));
#31290=CARTESIAN_POINT('Ctrl Pts',(-7.44466525340957,-0.588212004767528,
17.2560277573908));
#31291=CARTESIAN_POINT('Ctrl Pts',(-7.2921443747571,-0.0284493380852384,
17.2791816782399));
#31292=CARTESIAN_POINT('Ctrl Pts',(-7.4181416888383,0.537872733385351,17.302335599089));
#31293=CARTESIAN_POINT('Ctrl Pts',(-7.79360407735479,0.980168759268893,
17.3254895199381));
#31294=CARTESIAN_POINT('Ctrl Pts',(-8.33195287330967,1.19644525721016,17.3486434407872));
#31295=CARTESIAN_POINT('Ctrl Pts',(-8.90905292699061,1.13684195129112,17.3717973616362));
#31296=CARTESIAN_POINT('Ctrl Pts',(-9.39182556904706,0.815080213693786,
17.3949512824853));
#31297=CARTESIAN_POINT('Ctrl Pts',(-9.66895787403142,0.305406729054712,
17.4181052033344));
#31298=CARTESIAN_POINT('Ctrl Pts',(-9.67651470180108,-0.274755632204714,
17.4412591241835));
#31299=CARTESIAN_POINT('Ctrl Pts',(-9.5006889891414,-0.619153746004135,
17.4566950714162));
#31300=CARTESIAN_POINT('Ctrl Pts',(-9.37767319112126,-0.761025107359451,
17.4644130450326));
#31301=CARTESIAN_POINT('Ctrl Pts',(-8.78594175781903,1.06827677035486,16.1355869549674));
#31302=CARTESIAN_POINT('Ctrl Pts',(-8.95862320832669,1.02205575453656,16.1433049285838));
#31303=CARTESIAN_POINT('Ctrl Pts',(-9.28099614558818,0.844334504359283,
16.1587408758165));
#31304=CARTESIAN_POINT('Ctrl Pts',(-9.58457504934491,0.382890995678119,
16.1818947966656));
#31305=CARTESIAN_POINT('Ctrl Pts',(-9.63800694879561,-0.166805585848624,
16.2050487175147));
#31306=CARTESIAN_POINT('Ctrl Pts',(-9.42905039700147,-0.678065059187875,
16.2282026383638));
#31307=CARTESIAN_POINT('Ctrl Pts',(-9.00585354743959,-1.03296051556415,
16.2513565592128));
#31308=CARTESIAN_POINT('Ctrl Pts',(-8.46601746959882,-1.14967163652785,
16.2745104800619));
#31309=CARTESIAN_POINT('Ctrl Pts',(-7.93401500947623,-1.0012788338637,16.297664400911));
#31310=CARTESIAN_POINT('Ctrl Pts',(-7.53252361083745,-0.622003081831582,
16.3208183217601));
#31311=CARTESIAN_POINT('Ctrl Pts',(-7.35412122991775,-0.0992997245173969,
16.3439722426092));
#31312=CARTESIAN_POINT('Ctrl Pts',(-7.43994624620145,0.446300848993395,
16.3671261634583));
#31313=CARTESIAN_POINT('Ctrl Pts',(-7.77020800876001,0.888989406302429,
16.3902800843074));
#31314=CARTESIAN_POINT('Ctrl Pts',(-8.26875190652608,1.12668664068011,16.4134340051565));
#31315=CARTESIAN_POINT('Ctrl Pts',(-8.82061907406296,1.10458222554434,16.4365879260055));
#31316=CARTESIAN_POINT('Ctrl Pts',(-9.29855498473327,0.8277731673935,16.4597418468546));
#31317=CARTESIAN_POINT('Ctrl Pts',(-9.59235280674539,0.360088635071775,
16.4828957677037));
#31318=CARTESIAN_POINT('Ctrl Pts',(-9.63426596850247,-0.190628417505539,
16.5060496885528));
#31319=CARTESIAN_POINT('Ctrl Pts',(-9.41462974810337,-0.697388631836621,
16.5292036094019));
#31320=CARTESIAN_POINT('Ctrl Pts',(-8.98408986779299,-1.04333862207067,
16.552357530251));
#31321=CARTESIAN_POINT('Ctrl Pts',(-8.44192413508167,-1.14870608692133,
16.5755114511001));
#31322=CARTESIAN_POINT('Ctrl Pts',(-7.91315006452214,-0.989194436649623,
16.5986653719491));
#31323=CARTESIAN_POINT('Ctrl Pts',(-7.51969719874356,-0.601585320727254,
16.6218192927982));
#31324=CARTESIAN_POINT('Ctrl Pts',(-7.35229148429449,-0.0752571806156001,
16.6449732136473));
#31325=CARTESIAN_POINT('Ctrl Pts',(-7.44953485599114,0.468424445868551,
16.6681271344964));
#31326=CARTESIAN_POINT('Ctrl Pts',(-7.78900405123157,0.904092495873778,
16.6912810553455));
#31327=CARTESIAN_POINT('Ctrl Pts',(-8.29242117011678,1.13128666112824,16.7144349761946));
#31328=CARTESIAN_POINT('Ctrl Pts',(-8.84370370681767,1.09761844107208,16.7375888970437));
#31329=CARTESIAN_POINT('Ctrl Pts',(-9.31573191136605,0.810851360633317,
16.7607428178928));
#31330=CARTESIAN_POINT('Ctrl Pts',(-9.59966121977809,0.3371107859118,16.7838967387418));
#31331=CARTESIAN_POINT('Ctrl Pts',(-9.63002062528153,-0.21436386519221,
16.8070506595909));
#31332=CARTESIAN_POINT('Ctrl Pts',(-9.39980957955552,-0.716408543222247,
16.83020458044));
#31333=CARTESIAN_POINT('Ctrl Pts',(-8.96211224294239,-1.05325721226352,
16.8533585012891));
#31334=CARTESIAN_POINT('Ctrl Pts',(-8.41785685511504,-1.14723623722789,
16.8765124221382));
#31335=CARTESIAN_POINT('Ctrl Pts',(-7.89254278202879,-0.976675078313916,
16.8996663429873));
#31336=CARTESIAN_POINT('Ctrl Pts',(-7.50730172871725,-0.580903281493062,
16.9228202638364));
#31337=CARTESIAN_POINT('Ctrl Pts',(-7.35096608712355,-0.0511815135137962,
16.9459741846855));
#31338=CARTESIAN_POINT('Ctrl Pts',(-7.45958515384652,0.490342154186633,
16.9691281055345));
#31339=CARTESIAN_POINT('Ctrl Pts',(-7.80811255484906,0.918798260478664,
16.9922820263836));
#31340=CARTESIAN_POINT('Ctrl Pts',(-8.31618166666894,1.1353894929651,17.0154359472327));
#31341=CARTESIAN_POINT('Ctrl Pts',(-8.86663728446618,1.09017227151027,17.0385898680818));
#31342=CARTESIAN_POINT('Ctrl Pts',(-9.3325503369717,0.793573195913151,17.0617437889309));
#31343=CARTESIAN_POINT('Ctrl Pts',(-9.60648634723204,0.313984781321469,
17.08489770978));
#31344=CARTESIAN_POINT('Ctrl Pts',(-9.62527865516907,-0.238005101877905,
17.1080516306291));
#31345=CARTESIAN_POINT('Ctrl Pts',(-9.3845939571199,-0.735113606640794,
17.1312055514782));
#31346=CARTESIAN_POINT('Ctrl Pts',(-8.93993152812788,-1.06271290458967,
17.1543594723272));
#31347=CARTESIAN_POINT('Ctrl Pts',(-8.39382567246804,-1.14526220891511,
17.1775133931763));
#31348=CARTESIAN_POINT('Ctrl Pts',(-7.87220247515956,-0.963726453179972,
17.2006673140254));
#31349=CARTESIAN_POINT('Ctrl Pts',(-7.49534251878745,-0.559966013663411,
17.2238212348745));
#31350=CARTESIAN_POINT('Ctrl Pts',(-7.35014570585736,-0.0270831984213753,
17.2469751557236));
#31351=CARTESIAN_POINT('Ctrl Pts',(-7.47009261807012,0.512044038426373,
17.2701290765727));
#31352=CARTESIAN_POINT('Ctrl Pts',(-7.82752527036905,0.933100971072724,
17.2932829974218));
#31353=CARTESIAN_POINT('Ctrl Pts',(-8.34002251079937,1.13899185296508,17.3164369182709));
#31354=CARTESIAN_POINT('Ctrl Pts',(-8.88941017022393,1.08225070292711,17.3395908391199));
#31355=CARTESIAN_POINT('Ctrl Pts',(-9.34900002845021,0.775939991667486,
17.362744759969));
#31356=CARTESIAN_POINT('Ctrl Pts',(-9.61282441629278,0.290741071635111,
17.3858986808181));
#31357=CARTESIAN_POINT('Ctrl Pts',(-9.62001836454243,-0.261561843094395,
17.4090526016672));
#31358=CARTESIAN_POINT('Ctrl Pts',(-9.4526358177403,-0.589421929822272,
17.4244885488999));
#31359=CARTESIAN_POINT('Ctrl Pts',(-9.33552724893069,-0.724480616192563,
17.4322065225163));
#31360=CARTESIAN_POINT('Ctrl Pts',(-8.77151818897632,1.01439039972538,16.1033804324511));
#31361=CARTESIAN_POINT('Ctrl Pts',(-8.93548918457087,0.970500879693913,
16.1110984060675));
#31362=CARTESIAN_POINT('Ctrl Pts',(-9.24160087937137,0.8017443036737,16.1265343533002));
#31363=CARTESIAN_POINT('Ctrl Pts',(-9.52986655552915,0.363577081272822,
16.1496882741493));
#31364=CARTESIAN_POINT('Ctrl Pts',(-9.58060322541281,-0.158391523246551,
16.1728421949984));
#31365=CARTESIAN_POINT('Ctrl Pts',(-9.38218692920402,-0.643861876918772,
16.1959961158475));
#31366=CARTESIAN_POINT('Ctrl Pts',(-8.98033711527706,-0.980855579154441,
16.2191500366966));
#31367=CARTESIAN_POINT('Ctrl Pts',(-8.46773162765124,-1.09167951910348,
16.2423039575456));
#31368=CARTESIAN_POINT('Ctrl Pts',(-7.96256461180444,-0.950771995334296,
16.2654578783947));
#31369=CARTESIAN_POINT('Ctrl Pts',(-7.58132537525694,-0.590627796390225,
16.2886117992438));
#31370=CARTESIAN_POINT('Ctrl Pts',(-7.41192202631679,-0.0942908149283849,
16.3117657200929));
#31371=CARTESIAN_POINT('Ctrl Pts',(-7.49341782870659,0.423788393767846,
16.334919640942));
#31372=CARTESIAN_POINT('Ctrl Pts',(-7.807020418066,0.844146708264748,16.3580735617911));
#31373=CARTESIAN_POINT('Ctrl Pts',(-8.28041659943909,1.0698539400282,16.3812274826402));
#31374=CARTESIAN_POINT('Ctrl Pts',(-8.80444630055025,1.04886452312099,16.4043814034892));
#31375=CARTESIAN_POINT('Ctrl Pts',(-9.25827400973738,0.786018359151732,
16.4275353243383));
#31376=CARTESIAN_POINT('Ctrl Pts',(-9.53725198471509,0.341924924891599,
16.4506892451874));
#31377=CARTESIAN_POINT('Ctrl Pts',(-9.57705094888651,-0.181012675739665,
16.4738431660365));
#31378=CARTESIAN_POINT('Ctrl Pts',(-9.36849369145331,-0.662210723516617,
16.4969970868856));
#31379=CARTESIAN_POINT('Ctrl Pts',(-8.95967124636663,-0.990710189775668,
16.5201510077347));
#31380=CARTESIAN_POINT('Ctrl Pts',(-8.44485361709276,-1.09076267406997,
16.5433049285838));
#31381=CARTESIAN_POINT('Ctrl Pts',(-7.94275214331352,-0.939297163286455,
16.5664588494329));
#31382=CARTESIAN_POINT('Ctrl Pts',(-7.5691459572896,-0.571239954753235,
16.5896127702819));
#31383=CARTESIAN_POINT('Ctrl Pts',(-7.41018457732821,-0.071461032988207,
16.612766691131));
#31384=CARTESIAN_POINT('Ctrl Pts',(-7.50252276666583,0.444796024842794,
16.6359206119801));
#31385=CARTESIAN_POINT('Ctrl Pts',(-7.82486834433855,0.858487962790278,
16.6590745328292));
#31386=CARTESIAN_POINT('Ctrl Pts',(-8.30289193019724,1.0742219247215,16.6822284536783));
#31387=CARTESIAN_POINT('Ctrl Pts',(-8.82636649061465,1.04225200817126,16.7053823745274));
#31388=CARTESIAN_POINT('Ctrl Pts',(-9.2745844921485,0.769950127772109,16.7285362953765));
#31389=CARTESIAN_POINT('Ctrl Pts',(-9.54419174435727,0.320106132008483,
16.7516902162256));
#31390=CARTESIAN_POINT('Ctrl Pts',(-9.57301975067424,-0.2035508521137,16.7748441370746));
#31391=CARTESIAN_POINT('Ctrl Pts',(-9.35442108675531,-0.680271226233341,
16.7979980579237));
#31392=CARTESIAN_POINT('Ctrl Pts',(-8.93880222414703,-1.00012846315729,
16.8211519787728));
#31393=CARTESIAN_POINT('Ctrl Pts',(-8.42200034683252,-1.08936696702154,
16.8443058996219));
#31394=CARTESIAN_POINT('Ctrl Pts',(-7.92318434018817,-0.92740931056993,
16.867459820471));
#31395=CARTESIAN_POINT('Ctrl Pts',(-7.55737574366735,-0.551601165791326,
16.8906137413201));
#31396=CARTESIAN_POINT('Ctrl Pts',(-7.40892603628029,-0.0485997986594464,
16.9137676621692));
#31397=CARTESIAN_POINT('Ctrl Pts',(-7.51206610406846,0.465608152859449,
16.9369215830182));
#31398=CARTESIAN_POINT('Ctrl Pts',(-7.84301297048845,0.872451934346883,
16.9600755038674));
#31399=CARTESIAN_POINT('Ctrl Pts',(-8.3254538919136,1.07811780015612,16.9832294247164));
#31400=CARTESIAN_POINT('Ctrl Pts',(-8.84814324514455,1.03518144076042,17.0063833455655));
#31401=CARTESIAN_POINT('Ctrl Pts',(-9.29055455716002,0.753543513958735,
17.0295372664146));
#31402=CARTESIAN_POINT('Ctrl Pts',(-9.55067259647192,0.298146657000293,
17.0526911872637));
#31403=CARTESIAN_POINT('Ctrl Pts',(-9.56851697658858,-0.225999569709272,
17.0758451081128));
#31404=CARTESIAN_POINT('Ctrl Pts',(-9.33997297578552,-0.698032762648408,
17.0989990289619));
#31405=CARTESIAN_POINT('Ctrl Pts',(-8.91774035629475,-1.0091071883197,17.122152949811));
#31406=CARTESIAN_POINT('Ctrl Pts',(-8.39918135305896,-1.08749251329865,
17.14530687066));
#31407=CARTESIAN_POINT('Ctrl Pts',(-7.90387004581411,-0.915113844273164,
17.1684607915091));
#31408=CARTESIAN_POINT('Ctrl Pts',(-7.54601978416533,-0.531720022559295,
17.1916147123582));
#31409=CARTESIAN_POINT('Ctrl Pts',(-7.40814703695762,-0.0257170587575114,
17.2147686332073));
#31410=CARTESIAN_POINT('Ctrl Pts',(-7.52204354730195,0.486215343467395,
17.2379225540564));
#31411=CARTESIAN_POINT('Ctrl Pts',(-7.8614464633833,0.886033182876555,17.2610764749055));
#31412=CARTESIAN_POINT('Ctrl Pts',(-8.34809214828908,1.08153844871999,17.2842303957546));
#31413=CARTESIAN_POINT('Ctrl Pts',(-8.86976741345725,1.0276594545631,17.3073843166036));
#31414=CARTESIAN_POINT('Ctrl Pts',(-9.30617448785336,0.736799769641186,
17.3305382374527));
#31415=CARTESIAN_POINT('Ctrl Pts',(-9.55669095855414,0.276075414215511,
17.3536921583018));
#31416=CARTESIAN_POINT('Ctrl Pts',(-9.56352202728377,-0.248368053984077,
17.3768460791509));
#31417=CARTESIAN_POINT('Ctrl Pts',(-9.40458264633921,-0.559690113640409,
17.3922820263836));
#31418=CARTESIAN_POINT('Ctrl Pts',(-9.29338130674012,-0.687936125025675,
17.4));
#31419=CARTESIAN_POINT('Ctrl Pts',(-9.29338130674012,-0.687936125025675,
17.4));
#31420=CARTESIAN_POINT('Ctrl Pts',(-9.32590176996881,-0.655901643534808,
17.4));
#31421=CARTESIAN_POINT('Ctrl Pts',(-9.35618622301351,-0.62180741134238,
17.4));
#31422=CARTESIAN_POINT('Ctrl Pts',(-9.38414424671855,-0.585952842595447,
17.4));
#31423=CARTESIAN_POINT('Ctrl Pts',(-9.4125008379239,-0.549587133791166,
17.4));
#31424=CARTESIAN_POINT('Ctrl Pts',(-9.43846492414375,-0.511409752766397,
17.4));
#31425=CARTESIAN_POINT('Ctrl Pts',(-9.46191181465167,-0.47168786456472,
17.4));
#31426=CARTESIAN_POINT('Ctrl Pts',(-9.48267340922677,-0.436515194725088,
17.4));
#31427=CARTESIAN_POINT('Ctrl Pts',(-9.50146125422009,-0.400130473259426,
17.4));
#31428=CARTESIAN_POINT('Ctrl Pts',(-9.51816231358404,-0.362698001012095,
17.4));
#31429=CARTESIAN_POINT('Ctrl Pts',(-9.5228893675798,-0.35210314510194,17.4));
#31430=CARTESIAN_POINT('Ctrl Pts',(-9.52745040342208,-0.341420545917971,
17.4));
#31431=CARTESIAN_POINT('Ctrl Pts',(-9.53183247069625,-0.330679485922838,
17.4));
#31432=CARTESIAN_POINT('Ctrl Pts',(-9.54293259714113,-0.303471522959637,
17.4));
#31433=CARTESIAN_POINT('Ctrl Pts',(-9.55289892765706,-0.275859109257066,
17.4));
#31434=CARTESIAN_POINT('Ctrl Pts',(-9.56170405990825,-0.247910866813315,
17.4));
#31435=CARTESIAN_POINT('Ctrl Pts',(-9.57582363811113,-0.203094118630554,
17.4));
#31436=CARTESIAN_POINT('Ctrl Pts',(-9.5869600387577,-0.157414951204697,
17.4));
#31437=CARTESIAN_POINT('Ctrl Pts',(-9.59514858605679,-0.11117684925936,
17.4));
#31438=CARTESIAN_POINT('Ctrl Pts',(-9.60093527178937,-0.0785012897179607,
17.4));
#31439=CARTESIAN_POINT('Ctrl Pts',(-9.60524884863469,-0.0455458605504793,
17.4));
#31440=CARTESIAN_POINT('Ctrl Pts',(-9.60808714557939,-0.0124118703443701,
17.4));
#31441=CARTESIAN_POINT('Ctrl Pts',(-9.60984578868126,0.00811835057634134,
17.4));
#31442=CARTESIAN_POINT('Ctrl Pts',(-9.61103780203869,0.0287172011838359,
17.4));
#31443=CARTESIAN_POINT('Ctrl Pts',(-9.61166024116134,0.0493609406537205,
17.4));
#31444=CARTESIAN_POINT('Ctrl Pts',(-9.61202238478416,0.0613717515557251,
17.4));
#31445=CARTESIAN_POINT('Ctrl Pts',(-9.61219151258125,0.0734021836547561,
17.4));
#31446=CARTESIAN_POINT('Ctrl Pts',(-9.61216730618328,0.0854187262189934,
17.4));
#31447=CARTESIAN_POINT('Ctrl Pts',(-9.61206992538845,0.133760510359393,
17.4));
#31448=CARTESIAN_POINT('Ctrl Pts',(-9.60885229506756,0.181958671365902,
17.4));
#31449=CARTESIAN_POINT('Ctrl Pts',(-9.60254662600539,0.229702232680448,
17.4));
#31450=CARTESIAN_POINT('Ctrl Pts',(-9.60006992548072,0.24845464454845,17.4));
#31451=CARTESIAN_POINT('Ctrl Pts',(-9.5971162878431,0.267137112035182,17.4));
#31452=CARTESIAN_POINT('Ctrl Pts',(-9.59368553269945,0.285731284573432,
17.4));
#31453=CARTESIAN_POINT('Ctrl Pts',(-9.5852454443577,0.331475283283206,17.4));
#31454=CARTESIAN_POINT('Ctrl Pts',(-9.57392096633328,0.376685332484621,
17.4));
#31455=CARTESIAN_POINT('Ctrl Pts',(-9.55984225277605,0.421131437658512,
17.4));
#31456=CARTESIAN_POINT('Ctrl Pts',(-9.55380201884681,0.440200287337304,
17.4));
#31457=CARTESIAN_POINT('Ctrl Pts',(-9.54725424072087,0.459128450126187,
17.4));
#31458=CARTESIAN_POINT('Ctrl Pts',(-9.54020669887975,0.477897185647727,
17.4));
#31459=CARTESIAN_POINT('Ctrl Pts',(-9.53575786357977,0.489745148385171,
17.4));
#31460=CARTESIAN_POINT('Ctrl Pts',(-9.53110771266445,0.501534287767251,
17.4));
#31461=CARTESIAN_POINT('Ctrl Pts',(-9.52627028529036,0.513231192847217,
17.4));
#31462=CARTESIAN_POINT('Ctrl Pts',(-9.50753196688913,0.55854046878,17.4));
#31463=CARTESIAN_POINT('Ctrl Pts',(-9.48596288400885,0.602539245716482,
17.4));
#31464=CARTESIAN_POINT('Ctrl Pts',(-9.4617429788619,0.644973581298068,17.4));
#31465=CARTESIAN_POINT('Ctrl Pts',(-9.43730203087857,0.68779519361917,17.4));
#31466=CARTESIAN_POINT('Ctrl Pts',(-9.41016133012676,0.729024761307237,
17.4));
#31467=CARTESIAN_POINT('Ctrl Pts',(-9.38045491388209,0.768389604166219,
17.4));
#31468=CARTESIAN_POINT('Ctrl Pts',(-9.37505708296658,0.775542428122443,
17.4));
#31469=CARTESIAN_POINT('Ctrl Pts',(-9.36957441312197,0.782633627909684,
17.4));
#31470=CARTESIAN_POINT('Ctrl Pts',(-9.36400754339436,0.789661482345399,
17.4));
#31471=CARTESIAN_POINT('Ctrl Pts',(-9.34883017800262,0.808822037542452,
17.4));
#31472=CARTESIAN_POINT('Ctrl Pts',(-9.33302712271578,0.827511885585166,
17.4));
#31473=CARTESIAN_POINT('Ctrl Pts',(-9.31662661954985,0.845710363584338,
17.4));
#31474=CARTESIAN_POINT('Ctrl Pts',(-9.30887448664654,0.854312356990281,
17.4));
#31475=CARTESIAN_POINT('Ctrl Pts',(-9.30098883427567,0.862804538007458,
17.4));
#31476=CARTESIAN_POINT('Ctrl Pts',(-9.29297246379625,0.871184557480965,
17.4));
#31477=CARTESIAN_POINT('Ctrl Pts',(-9.2855447605525,0.878949205832212,17.4));
#31478=CARTESIAN_POINT('Ctrl Pts',(-9.27801053976762,0.886611521389777,
17.4));
#31479=CARTESIAN_POINT('Ctrl Pts',(-9.27037638926497,0.894166318207978,
17.4));
#31480=CARTESIAN_POINT('Ctrl Pts',(-9.23471836479337,0.92945369297585,17.4));
#31481=CARTESIAN_POINT('Ctrl Pts',(-9.19685839181085,0.962424199673336,
17.4));
#31482=CARTESIAN_POINT('Ctrl Pts',(-9.15706782341478,0.992922306002667,
17.4));
#31483=CARTESIAN_POINT('Ctrl Pts',(-9.1348200157453,1.00997448774444,17.4));
#31484=CARTESIAN_POINT('Ctrl Pts',(-9.11196784459699,1.02625325759119,17.4));
#31485=CARTESIAN_POINT('Ctrl Pts',(-9.08855339782672,1.04172681883086,17.4));
#31486=CARTESIAN_POINT('Ctrl Pts',(-9.07636602844239,1.04978090647893,17.4));
#31487=CARTESIAN_POINT('Ctrl Pts',(-9.06402403497495,1.05761791257647,17.4));
#31488=CARTESIAN_POINT('Ctrl Pts',(-9.05155345664447,1.06522115394551,17.4));
#31489=CARTESIAN_POINT('Ctrl Pts',(-9.00599344516773,1.09299883633154,17.4));
#31490=CARTESIAN_POINT('Ctrl Pts',(-8.95866633005178,1.11769733240675,17.4));
#31491=CARTESIAN_POINT('Ctrl Pts',(-8.90987139744227,1.13911609011303,17.4));
#31492=CARTESIAN_POINT('Ctrl Pts',(-8.87875620954714,1.15277424342671,17.4));
#31493=CARTESIAN_POINT('Ctrl Pts',(-8.84704320481553,1.16509794048545,17.4));
#31494=CARTESIAN_POINT('Ctrl Pts',(-8.81482206889638,1.17607882593351,17.4));
#31495=CARTESIAN_POINT('Ctrl Pts',(-9.55005247215833,-1.9100347204657E-5,
16.4658930328476));
#31496=CARTESIAN_POINT('Ctrl Pts',(-9.55009316010148,-0.0583092136036194,
16.4685430772439));
#31497=CARTESIAN_POINT('Ctrl Pts',(-9.54531572343602,-0.116592726407586,
16.4711931216402));
#31498=CARTESIAN_POINT('Ctrl Pts',(-9.53565824528574,-0.174056083597285,
16.4738431660365));
#31499=CARTESIAN_POINT('Ctrl Pts',(-9.50753186307544,-0.341412024998651,
16.4815611396529));
#31500=CARTESIAN_POINT('Ctrl Pts',(-9.43801277726438,-0.501811374257632,
16.4892791132692));
#31501=CARTESIAN_POINT('Ctrl Pts',(-9.33511616017773,-0.636760959930297,
16.4969970868856));
#31502=CARTESIAN_POINT('Ctrl Pts',(-9.23221954309108,-0.771710545602965,
16.504715060502));
#31503=CARTESIAN_POINT('Ctrl Pts',(-9.09594539472886,-0.881210367689316,
16.5124330341183));
#31504=CARTESIAN_POINT('Ctrl Pts',(-8.94200538233543,-0.952635692781543,
16.5201510077347));
#31505=CARTESIAN_POINT('Ctrl Pts',(-8.78806536994201,-1.02406101787377,
16.527868981351));
#31506=CARTESIAN_POINT('Ctrl Pts',(-8.61645949351738,-1.05741184597187,
16.5355869549674));
#31507=CARTESIAN_POINT('Ctrl Pts',(-8.44697297634186,-1.04884300822367,
16.5433049285838));
#31508=CARTESIAN_POINT('Ctrl Pts',(-8.27748645916635,-1.04027417047547,
16.5510229022001));
#31509=CARTESIAN_POINT('Ctrl Pts',(-8.11011930123993,-0.98978566688096,
16.5587408758165));
#31510=CARTESIAN_POINT('Ctrl Pts',(-7.96416802460607,-0.903198546994836,
16.5664588494329));
#31511=CARTESIAN_POINT('Ctrl Pts',(-7.81821674797221,-0.816611427108713,
16.5741768230492));
#31512=CARTESIAN_POINT('Ctrl Pts',(-7.6936813526309,-0.693925690930975,
16.5818947966656));
#31513=CARTESIAN_POINT('Ctrl Pts',(-7.60492009163335,-0.549286335881268,
16.5896127702819));
#31514=CARTESIAN_POINT('Ctrl Pts',(-7.5161588306358,-0.404646980831559,
16.5973307438983));
#31515=CARTESIAN_POINT('Ctrl Pts',(-7.463171703982,-0.238054006909883,16.6050487175147));
#31516=CARTESIAN_POINT('Ctrl Pts',(-7.45206783887804,-0.0687146769772104,
16.612766691131));
#31517=CARTESIAN_POINT('Ctrl Pts',(-7.44096397377408,0.100624652955459,
16.6204846647474));
#31518=CARTESIAN_POINT('Ctrl Pts',(-7.47174337021995,0.272710338899125,
16.6282026383638));
#31519=CARTESIAN_POINT('Ctrl Pts',(-7.54085733138834,0.427701838195537,
16.6359206119801));
#31520=CARTESIAN_POINT('Ctrl Pts',(-7.60997129255673,0.582693337491953,
16.6436385855965));
#31521=CARTESIAN_POINT('Ctrl Pts',(-7.71741981844764,0.720590650141115,
16.6513565592128));
#31522=CARTESIAN_POINT('Ctrl Pts',(-7.85081467903621,0.825494966787567,
16.6590745328292));
#31523=CARTESIAN_POINT('Ctrl Pts',(-7.98420953962478,0.930399283434019,
16.6667925064456));
#31524=CARTESIAN_POINT('Ctrl Pts',(-8.14355073491101,1.00231060407776,16.6745104800619));
#31525=CARTESIAN_POINT('Ctrl Pts',(-8.3104670926237,1.03293794497459,16.6822284536783));
#31526=CARTESIAN_POINT('Ctrl Pts',(-8.47738345033638,1.06356528587142,16.6899464272947));
#31527=CARTESIAN_POINT('Ctrl Pts',(-8.65187497047551,1.05290864702134,16.697664400911));
#31528=CARTESIAN_POINT('Ctrl Pts',(-8.81382373080072,1.00219668086311,16.7053823745274));
#31529=CARTESIAN_POINT('Ctrl Pts',(-8.97577249112593,0.951484714704877,
16.7131003481437));
#31530=CARTESIAN_POINT('Ctrl Pts',(-9.12517849163721,0.860717421238493,
16.7208183217601));
#31531=CARTESIAN_POINT('Ctrl Pts',(-9.24481603392765,0.740359775211364,
16.7285362953765));
#31532=CARTESIAN_POINT('Ctrl Pts',(-9.36445357621809,0.620002129184234,
16.7362542689928));
#31533=CARTESIAN_POINT('Ctrl Pts',(-9.45432266028768,0.470054130596359,
16.7439722426092));
#31534=CARTESIAN_POINT('Ctrl Pts',(-9.50406187004197,0.307803967282058,
16.7516902162256));
#31535=CARTESIAN_POINT('Ctrl Pts',(-9.5345723343245,0.208278304588784,16.7564244884329));
#31536=CARTESIAN_POINT('Ctrl Pts',(-9.54998312115351,0.104123703417168,
16.7611587606403));
#31537=CARTESIAN_POINT('Ctrl Pts',(-9.55003851802847,-1.48519297202892E-5,
16.7658930328476));
#31538=CARTESIAN_POINT('Ctrl Pts',(-8.81478889550445,1.17604951161381,16.2));
#31539=CARTESIAN_POINT('Ctrl Pts',(-8.86280065303638,1.1596386364084,16.2));
#31540=CARTESIAN_POINT('Ctrl Pts',(-8.90960823495586,1.14022110609085,16.2));
#31541=CARTESIAN_POINT('Ctrl Pts',(-8.9549737777663,1.11798780847924,16.2));
#31542=CARTESIAN_POINT('Ctrl Pts',(-9.00031713849028,1.09576538213465,16.2));
#31543=CARTESIAN_POINT('Ctrl Pts',(-9.04422076807012,1.07072924115979,16.2));
#31544=CARTESIAN_POINT('Ctrl Pts',(-9.08641991384138,1.04302575780302,16.2));
#31545=CARTESIAN_POINT('Ctrl Pts',(-9.1251986712936,1.01756773864081,16.2));
#31546=CARTESIAN_POINT('Ctrl Pts',(-9.16253828107189,0.989856378454144,
16.2));
#31547=CARTESIAN_POINT('Ctrl Pts',(-9.19820325527869,0.959979731284522,
16.2));
#31548=CARTESIAN_POINT('Ctrl Pts',(-9.20529901205526,0.954035596280082,
16.2));
#31549=CARTESIAN_POINT('Ctrl Pts',(-9.21233002234639,0.948004232316305,
16.2));
#31550=CARTESIAN_POINT('Ctrl Pts',(-9.2192889249183,0.941890947120833,16.2));
#31551=CARTESIAN_POINT('Ctrl Pts',(-9.24730713452057,0.917277395746144,
16.2));
#31552=CARTESIAN_POINT('Ctrl Pts',(-9.27408780072704,0.891399085013077,
16.2));
#31553=CARTESIAN_POINT('Ctrl Pts',(-9.29952946398766,0.864320328704408,
16.2));
#31554=CARTESIAN_POINT('Ctrl Pts',(-9.33347386455,0.828191710010907,16.2));
#31555=CARTESIAN_POINT('Ctrl Pts',(-9.36503664794811,0.789926769837996,
16.2));
#31556=CARTESIAN_POINT('Ctrl Pts',(-9.39406804371783,0.749791809119003,
16.2));
#31557=CARTESIAN_POINT('Ctrl Pts',(-9.41426326769662,0.7218725685999,16.2));
#31558=CARTESIAN_POINT('Ctrl Pts',(-9.43323268273991,0.693047684123375,
16.2));
#31559=CARTESIAN_POINT('Ctrl Pts',(-9.45091216409187,0.663401052699072,
16.2));
#31560=CARTESIAN_POINT('Ctrl Pts',(-9.46034291018765,0.647586683035633,
16.2));
#31561=CARTESIAN_POINT('Ctrl Pts',(-9.46940640954167,0.631538429490315,
16.2));
#31562=CARTESIAN_POINT('Ctrl Pts',(-9.47809147938961,0.615268771658106,
16.2));
#31563=CARTESIAN_POINT('Ctrl Pts',(-9.48251125162093,0.606989254836849,
16.2));
#31564=CARTESIAN_POINT('Ctrl Pts',(-9.48683300444743,0.598652398763581,
16.2));
#31565=CARTESIAN_POINT('Ctrl Pts',(-9.49105515788789,0.590259842587576,
16.2));
#31566=CARTESIAN_POINT('Ctrl Pts',(-9.49557721907162,0.581271146877932,
16.2));
#31567=CARTESIAN_POINT('Ctrl Pts',(-9.49998165828265,0.572225103576722,
16.2));
#31568=CARTESIAN_POINT('Ctrl Pts',(-9.50426374372789,0.563131296471702,
16.2));
#31569=CARTESIAN_POINT('Ctrl Pts',(-9.52493494242546,0.519232150602404,
16.2));
#31570=CARTESIAN_POINT('Ctrl Pts',(-9.54278537558293,0.474168676113686,
16.2));
#31571=CARTESIAN_POINT('Ctrl Pts',(-9.55766754962425,0.428188388568034,
16.2));
#31572=CARTESIAN_POINT('Ctrl Pts',(-9.56297844699411,0.411779724920264,
16.2));
#31573=CARTESIAN_POINT('Ctrl Pts',(-9.56791087712962,0.395254153812105,
16.2));
#31574=CARTESIAN_POINT('Ctrl Pts',(-9.57245656145425,0.378622557723441,
16.2));
#31575=CARTESIAN_POINT('Ctrl Pts',(-9.58437736922181,0.335007109381333,
16.2));
#31576=CARTESIAN_POINT('Ctrl Pts',(-9.59364121622314,0.290662195371642,
16.2));
#31577=CARTESIAN_POINT('Ctrl Pts',(-9.6002178916675,0.24583507512556,16.2));
#31578=CARTESIAN_POINT('Ctrl Pts',(-9.60298148599042,0.22699820593944,16.2));
#31579=CARTESIAN_POINT('Ctrl Pts',(-9.6052701103365,0.208076238849532,16.2));
#31580=CARTESIAN_POINT('Ctrl Pts',(-9.60707946344055,0.189087960713112,
16.2));
#31581=CARTESIAN_POINT('Ctrl Pts',(-9.6079693515963,0.179749018649314,16.2));
#31582=CARTESIAN_POINT('Ctrl Pts',(-9.60874342397162,0.170392071550278,
16.2));
#31583=CARTESIAN_POINT('Ctrl Pts',(-9.60940063069509,0.161025657024326,
16.2));
#31584=CARTESIAN_POINT('Ctrl Pts',(-9.61273662950675,0.113481487721126,
16.2));
#31585=CARTESIAN_POINT('Ctrl Pts',(-9.61305386042052,0.0658810798401326,
16.2));
#31586=CARTESIAN_POINT('Ctrl Pts',(-9.6103549875713,0.0185133182208896,
16.2));
#31587=CARTESIAN_POINT('Ctrl Pts',(-9.60768669390768,-0.0283177498764049,
16.2));
#31588=CARTESIAN_POINT('Ctrl Pts',(-9.60207007581538,-0.0749224868667112,
16.2));
#31589=CARTESIAN_POINT('Ctrl Pts',(-9.59345823475354,-0.121012650095075,
16.2));
#31590=CARTESIAN_POINT('Ctrl Pts',(-9.59107634935637,-0.133760387304665,
16.2));
#31591=CARTESIAN_POINT('Ctrl Pts',(-9.58846504996881,-0.146468654771097,
16.2));
#31592=CARTESIAN_POINT('Ctrl Pts',(-9.58562269218988,-0.159131062787288,
16.2));
#31593=CARTESIAN_POINT('Ctrl Pts',(-9.58068397833975,-0.181132518870406,
16.2));
#31594=CARTESIAN_POINT('Ctrl Pts',(-9.57504779217974,-0.202995620919267,
16.2));
#31595=CARTESIAN_POINT('Ctrl Pts',(-9.56872407785818,-0.22468856278884,
16.2));
#31596=CARTESIAN_POINT('Ctrl Pts',(-9.56551410869643,-0.235700077681537,
16.2));
#31597=CARTESIAN_POINT('Ctrl Pts',(-9.56212695335901,-0.246667721625346,
16.2));
#31598=CARTESIAN_POINT('Ctrl Pts',(-9.55856371499839,-0.257587153871304,
16.2));
#31599=CARTESIAN_POINT('Ctrl Pts',(-9.55533513157818,-0.267481046544088,
16.2));
#31600=CARTESIAN_POINT('Ctrl Pts',(-9.55196458780484,-0.277327250705073,
16.2));
#31601=CARTESIAN_POINT('Ctrl Pts',(-9.54845505697522,-0.287118724757319,
16.2));
#31602=CARTESIAN_POINT('Ctrl Pts',(-9.53268035933277,-0.331129605455121,
16.2));
#31603=CARTESIAN_POINT('Ctrl Pts',(-9.51409226223222,-0.374064154494532,
16.2));
#31604=CARTESIAN_POINT('Ctrl Pts',(-9.4928094624077,-0.415647754292589,
16.2));
#31605=CARTESIAN_POINT('Ctrl Pts',(-9.48095709789152,-0.438805608840179,
16.2));
#31606=CARTESIAN_POINT('Ctrl Pts',(-9.46826821755998,-0.461544009845136,
16.2));
#31607=CARTESIAN_POINT('Ctrl Pts',(-9.45475802396731,-0.483810850745379,
16.2));
#31608=CARTESIAN_POINT('Ctrl Pts',(-9.44902429640731,-0.493260900329658,
16.2));
#31609=CARTESIAN_POINT('Ctrl Pts',(-9.44314317361927,-0.502624771124578,
16.2));
#31610=CARTESIAN_POINT('Ctrl Pts',(-9.43712266825694,-0.511888352961157,
16.2));
#31611=CARTESIAN_POINT('Ctrl Pts',(-9.41182957357249,-0.550806124544883,
16.2));
#31612=CARTESIAN_POINT('Ctrl Pts',(-9.38404938266935,-0.588007231454378,
16.2));
#31613=CARTESIAN_POINT('Ctrl Pts',(-9.35388344975981,-0.623204450374551,
16.2));
#31614=CARTESIAN_POINT('Ctrl Pts',(-9.33467682049038,-0.645614496075499,
16.2));
#31615=CARTESIAN_POINT('Ctrl Pts',(-9.31450214867004,-0.667211421582346,
16.2));
#31616=CARTESIAN_POINT('Ctrl Pts',(-9.29341917486498,-0.68794102932241,
16.2));
#31617=CARTESIAN_POINT('Origin',(-8.5,0.,17.4));
#31618=CARTESIAN_POINT('',(-7.46076951545867,-1.8,17.4));
#31619=CARTESIAN_POINT('',(-6.42153903091735,0.,17.4));
#31620=CARTESIAN_POINT('',(-7.46076951545867,-1.8,17.4));
#31621=CARTESIAN_POINT('',(-7.46076951545867,1.8,17.4));
#31622=CARTESIAN_POINT('',(-6.42153903091735,0.,17.4));
#31623=CARTESIAN_POINT('',(-9.53923048454133,1.8,17.4));
#31624=CARTESIAN_POINT('',(-7.46076951545867,1.8,17.4));
#31625=CARTESIAN_POINT('',(-10.5784609690827,2.22044604925031E-16,17.4));
#31626=CARTESIAN_POINT('',(-9.53923048454133,1.8,17.4));
#31627=CARTESIAN_POINT('',(-9.53923048454133,-1.8,17.4));
#31628=CARTESIAN_POINT('',(-10.5784609690827,2.54538057293978E-16,17.4));
#31629=CARTESIAN_POINT('',(-9.53923048454133,-1.8,17.4));
#31630=CARTESIAN_POINT('Origin',(-8.5,0.,16.1));
#31631=CARTESIAN_POINT('Origin',(-9.53923048454133,-1.8,16.2));
#31632=CARTESIAN_POINT('',(-9.53923048454133,-1.8,16.2));
#31633=CARTESIAN_POINT('',(-7.46076951545867,-1.8,16.2));
#31634=CARTESIAN_POINT('',(-9.53923048454133,-1.8,16.2));
#31635=CARTESIAN_POINT('',(-7.46076951545867,-1.8,16.2));
#31636=CARTESIAN_POINT('',(-9.53923048454133,-1.8,16.2));
#31637=CARTESIAN_POINT('Origin',(-10.5784609690827,2.54538057293978E-16,
16.2));
#31638=CARTESIAN_POINT('',(-10.5784609690827,2.54538057293978E-16,16.2));
#31639=CARTESIAN_POINT('',(-10.5784609690827,2.54538057293978E-16,16.2));
#31640=CARTESIAN_POINT('',(-10.5784609690827,2.54538057293978E-16,16.2));
#31641=CARTESIAN_POINT('Origin',(-9.53923048454133,1.8,16.2));
#31642=CARTESIAN_POINT('',(-9.53923048454133,1.8,16.2));
#31643=CARTESIAN_POINT('',(-9.53923048454133,1.8,16.2));
#31644=CARTESIAN_POINT('',(-9.53923048454133,1.8,16.2));
#31645=CARTESIAN_POINT('Origin',(-7.46076951545867,1.8,16.2));
#31646=CARTESIAN_POINT('',(-7.46076951545867,1.8,16.2));
#31647=CARTESIAN_POINT('',(-7.46076951545867,1.8,16.2));
#31648=CARTESIAN_POINT('',(-7.46076951545867,1.8,16.2));
#31649=CARTESIAN_POINT('Origin',(-6.42153903091735,0.,16.2));
#31650=CARTESIAN_POINT('',(-6.42153903091735,0.,16.2));
#31651=CARTESIAN_POINT('',(-6.42153903091735,0.,16.2));
#31652=CARTESIAN_POINT('',(-6.42153903091735,0.,16.2));
#31653=CARTESIAN_POINT('Origin',(-7.46076951545867,-1.8,16.2));
#31654=CARTESIAN_POINT('',(-7.46076951545867,-1.8,16.2));
#31655=CARTESIAN_POINT('Origin',(-8.5,0.,16.2));
#34399=UNCERTAINTY_MEASURE_WITH_UNIT(LENGTH_MEASURE(0.001),#34434,
'DISTANCE_ACCURACY_VALUE',
'Maximum model space distance between geometric entities at asserted c
onnectivities');
#34404=UNCERTAINTY_MEASURE_WITH_UNIT(LENGTH_MEASURE(0.001),#34434,
'DISTANCE_ACCURACY_VALUE',
'Maximum model space distance between geometric entities at asserted c
onnectivities');
#34428=(
GEOMETRIC_REPRESENTATION_CONTEXT(3)
GLOBAL_UNCERTAINTY_ASSIGNED_CONTEXT((#34399))
GLOBAL_UNIT_ASSIGNED_CONTEXT((#34434,#34436,#34437))
REPRESENTATION_CONTEXT('','3D')
);
#34433=(
GEOMETRIC_REPRESENTATION_CONTEXT(3)
GLOBAL_UNCERTAINTY_ASSIGNED_CONTEXT((#34404))
GLOBAL_UNIT_ASSIGNED_CONTEXT((#34434,#34436,#34437))
REPRESENTATION_CONTEXT('','3D')
);
#34434=(
LENGTH_UNIT()
NAMED_UNIT(*)
SI_UNIT(.CENTI.,.METRE.)
);
#34436=(
NAMED_UNIT(*)
PLANE_ANGLE_UNIT()
SI_UNIT($,.RADIAN.)
);
#34437=(
NAMED_UNIT(*)
SI_UNIT($,.STERADIAN.)
SOLID_ANGLE_UNIT()
);
#34461=SHAPE_DEFINITION_REPRESENTATION(#34524,#34560);
#34524=PRODUCT_DEFINITION_SHAPE('',$,#34589);
#34560=SHAPE_REPRESENTATION('',(#9646),#34428);
#34565=PRODUCT_DEFINITION_CONTEXT('part definition',#34651,'design');
#34589=PRODUCT_DEFINITION('M24 adjustment nut (1)',
'M24 adjustment nut (1)',#34617,#34565);
#34617=PRODUCT_DEFINITION_FORMATION('',$,#34676);
#34651=APPLICATION_CONTEXT(
'Core Data for Automotive Mechanical Design Process');
#34652=PRODUCT_CONTEXT('part definition',#34651,'mechanical');
#34676=PRODUCT('M24 adjustment nut (1)','M24 adjustment nut (1)',
'M24 adjustment nut (1)',(#34652));
#34744=COLOUR_RGB('Black',0.12,0.14,0.17);
#34745=FILL_AREA_STYLE_COLOUR('',#34744);
#34746=FILL_AREA_STYLE('',(#34745));
#34747=SURFACE_STYLE_FILL_AREA(#34746);
#34748=SURFACE_SIDE_STYLE('',(#34747));
#34749=SURFACE_STYLE_USAGE(.BOTH.,#34748);
#34750=PRESENTATION_STYLE_ASSIGNMENT((#34749));
ENDSEC;
END-ISO-10303-21;
